ISO-10303-21;
HEADER;
/* Generated by software containing ST-Developer
 * from STEP Tools, Inc. (www.steptools.com) 
 */

FILE_DESCRIPTION(
/* description */ (''),
/* implementation_level */ '2;1');

FILE_NAME(
/* name */ '04_Journal_Retaining_Ring_D18.step',
/* time_stamp */ '2026-10-25T01:10:36-07:00',
/* author */ (''),
/* organization */ (''),
/* preprocessor_version */ 'ST-DEVELOPER v20.2',
/* originating_system */ 'Autodesk Translation Framework v15.15.0.0',
/* authorisation */ '');

FILE_SCHEMA (('AUTOMOTIVE_DESIGN { 1 0 10303 214 3 1 1 }'));
ENDSEC;

DATA;
#10=MECHANICAL_DESIGN_GEOMETRIC_PRESENTATION_REPRESENTATION('',(#1304),#60365);
#76=SHAPE_REPRESENTATION_RELATIONSHIP('SRR','None',#60416,#86);
#86=ADVANCED_BREP_SHAPE_REPRESENTATION('',(#96),#60364);
#96=MANIFOLD_SOLID_BREP('Body1',#18306);
#260=FACE_BOUND('',#3141,.T.);
#261=FACE_BOUND('',#3142,.T.);
#262=FACE_BOUND('',#3145,.T.);
#263=FACE_BOUND('',#3146,.T.);
#675=PLANE('',#19503);
#676=PLANE('',#19507);
#677=PLANE('',#19514);
#678=PLANE('',#19515);
#679=PLANE('',#19516);
#680=PLANE('',#19517);
#681=PLANE('',#19518);
#682=PLANE('',#19519);
#683=PLANE('',#19520);
#684=PLANE('',#19521);
#685=PLANE('',#19522);
#686=PLANE('',#19523);
#687=PLANE('',#19524);
#688=PLANE('',#19525);
#689=PLANE('',#19526);
#690=PLANE('',#19527);
#691=PLANE('',#19528);
#692=PLANE('',#19529);
#693=PLANE('',#19530);
#694=PLANE('',#19531);
#695=PLANE('',#19532);
#696=PLANE('',#19533);
#697=PLANE('',#19534);
#698=PLANE('',#19535);
#699=PLANE('',#19536);
#700=PLANE('',#19537);
#701=PLANE('',#19538);
#702=PLANE('',#19539);
#703=PLANE('',#19540);
#704=PLANE('',#19541);
#705=PLANE('',#19542);
#706=PLANE('',#19543);
#707=PLANE('',#19544);
#708=PLANE('',#19545);
#709=PLANE('',#19546);
#710=PLANE('',#19547);
#711=PLANE('',#19548);
#712=PLANE('',#19549);
#713=PLANE('',#19550);
#714=PLANE('',#19551);
#715=PLANE('',#19552);
#716=PLANE('',#19553);
#717=PLANE('',#19554);
#718=PLANE('',#19555);
#719=PLANE('',#19556);
#720=PLANE('',#19557);
#721=PLANE('',#19558);
#722=PLANE('',#19559);
#723=PLANE('',#19560);
#724=PLANE('',#19561);
#725=PLANE('',#19562);
#726=PLANE('',#19563);
#727=PLANE('',#19564);
#728=PLANE('',#19565);
#729=PLANE('',#19566);
#730=PLANE('',#19567);
#731=PLANE('',#19568);
#732=PLANE('',#19569);
#733=PLANE('',#19570);
#734=PLANE('',#19571);
#735=PLANE('',#19572);
#736=PLANE('',#19573);
#737=PLANE('',#19574);
#738=PLANE('',#19575);
#739=PLANE('',#19576);
#740=PLANE('',#19577);
#741=PLANE('',#19578);
#742=PLANE('',#19579);
#743=PLANE('',#19580);
#744=PLANE('',#19581);
#745=PLANE('',#19582);
#746=PLANE('',#19583);
#747=PLANE('',#19584);
#748=PLANE('',#19585);
#749=PLANE('',#19586);
#750=PLANE('',#19587);
#751=PLANE('',#19588);
#752=PLANE('',#19589);
#753=PLANE('',#19590);
#754=PLANE('',#19591);
#755=PLANE('',#19592);
#756=PLANE('',#19593);
#757=PLANE('',#19594);
#758=PLANE('',#19595);
#759=PLANE('',#19596);
#760=PLANE('',#19597);
#761=PLANE('',#19598);
#762=PLANE('',#19599);
#763=PLANE('',#19600);
#764=PLANE('',#19601);
#765=PLANE('',#19602);
#766=PLANE('',#19603);
#767=PLANE('',#19604);
#768=PLANE('',#19605);
#769=PLANE('',#19606);
#770=PLANE('',#19607);
#771=PLANE('',#19608);
#772=PLANE('',#19609);
#773=PLANE('',#19610);
#774=PLANE('',#19611);
#775=PLANE('',#19612);
#776=PLANE('',#19613);
#777=PLANE('',#19614);
#778=PLANE('',#19615);
#779=PLANE('',#19616);
#780=PLANE('',#19617);
#781=PLANE('',#19618);
#782=PLANE('',#19619);
#783=PLANE('',#19620);
#784=PLANE('',#19621);
#785=PLANE('',#19622);
#786=PLANE('',#19623);
#787=PLANE('',#19624);
#788=PLANE('',#19625);
#789=PLANE('',#19626);
#790=PLANE('',#19627);
#791=PLANE('',#19628);
#792=PLANE('',#19629);
#793=PLANE('',#19630);
#794=PLANE('',#19631);
#795=PLANE('',#19632);
#796=PLANE('',#19633);
#797=PLANE('',#19634);
#798=PLANE('',#19635);
#799=PLANE('',#19636);
#800=PLANE('',#19637);
#801=PLANE('',#19638);
#802=PLANE('',#19639);
#803=PLANE('',#19640);
#804=PLANE('',#19641);
#805=PLANE('',#19642);
#806=PLANE('',#19643);
#807=PLANE('',#19644);
#808=PLANE('',#19645);
#809=PLANE('',#19646);
#810=PLANE('',#19647);
#811=PLANE('',#19648);
#812=PLANE('',#19649);
#813=PLANE('',#19650);
#814=PLANE('',#19651);
#815=PLANE('',#19652);
#816=PLANE('',#19653);
#817=PLANE('',#19654);
#818=PLANE('',#19655);
#819=PLANE('',#19656);
#820=PLANE('',#19657);
#821=PLANE('',#19658);
#822=PLANE('',#19659);
#823=PLANE('',#19660);
#824=PLANE('',#19661);
#825=PLANE('',#19662);
#826=PLANE('',#19663);
#972=CONICAL_SURFACE('',#19498,0.650000000000001,0.785398163397449);
#973=CONICAL_SURFACE('',#19505,0.650000000000001,0.785398163397449);
#974=CONICAL_SURFACE('',#19509,0.650000000000001,0.785398163397449);
#975=CONICAL_SURFACE('',#19513,0.650000000000001,0.785398163397449);
#1304=STYLED_ITEM('',(#60541),#96);
#2111=FACE_OUTER_BOUND('',#3138,.T.);
#2112=FACE_OUTER_BOUND('',#3139,.T.);
#2113=FACE_OUTER_BOUND('',#3140,.T.);
#2114=FACE_OUTER_BOUND('',#3143,.T.);
#2115=FACE_OUTER_BOUND('',#3144,.T.);
#2116=FACE_OUTER_BOUND('',#3147,.T.);
#2117=FACE_OUTER_BOUND('',#3148,.T.);
#2118=FACE_OUTER_BOUND('',#3149,.T.);
#2119=FACE_OUTER_BOUND('',#3150,.T.);
#2120=FACE_OUTER_BOUND('',#3151,.T.);
#2121=FACE_OUTER_BOUND('',#3152,.T.);
#2122=FACE_OUTER_BOUND('',#3153,.T.);
#2123=FACE_OUTER_BOUND('',#3154,.T.);
#2124=FACE_OUTER_BOUND('',#3155,.T.);
#2125=FACE_OUTER_BOUND('',#3156,.T.);
#2126=FACE_OUTER_BOUND('',#3157,.T.);
#2127=FACE_OUTER_BOUND('',#3158,.T.);
#2128=FACE_OUTER_BOUND('',#3159,.T.);
#2129=FACE_OUTER_BOUND('',#3160,.T.);
#2130=FACE_OUTER_BOUND('',#3161,.T.);
#2131=FACE_OUTER_BOUND('',#3162,.T.);
#2132=FACE_OUTER_BOUND('',#3163,.T.);
#2133=FACE_OUTER_BOUND('',#3164,.T.);
#2134=FACE_OUTER_BOUND('',#3165,.T.);
#2135=FACE_OUTER_BOUND('',#3166,.T.);
#2136=FACE_OUTER_BOUND('',#3167,.T.);
#2137=FACE_OUTER_BOUND('',#3168,.T.);
#2138=FACE_OUTER_BOUND('',#3169,.T.);
#2139=FACE_OUTER_BOUND('',#3170,.T.);
#2140=FACE_OUTER_BOUND('',#3171,.T.);
#2141=FACE_OUTER_BOUND('',#3172,.T.);
#2142=FACE_OUTER_BOUND('',#3173,.T.);
#2143=FACE_OUTER_BOUND('',#3174,.T.);
#2144=FACE_OUTER_BOUND('',#3175,.T.);
#2145=FACE_OUTER_BOUND('',#3176,.T.);
#2146=FACE_OUTER_BOUND('',#3177,.T.);
#2147=FACE_OUTER_BOUND('',#3178,.T.);
#2148=FACE_OUTER_BOUND('',#3179,.T.);
#2149=FACE_OUTER_BOUND('',#3180,.T.);
#2150=FACE_OUTER_BOUND('',#3181,.T.);
#2151=FACE_OUTER_BOUND('',#3182,.T.);
#2152=FACE_OUTER_BOUND('',#3183,.T.);
#2153=FACE_OUTER_BOUND('',#3184,.T.);
#2154=FACE_OUTER_BOUND('',#3185,.T.);
#2155=FACE_OUTER_BOUND('',#3186,.T.);
#2156=FACE_OUTER_BOUND('',#3187,.T.);
#2157=FACE_OUTER_BOUND('',#3188,.T.);
#2158=FACE_OUTER_BOUND('',#3189,.T.);
#2159=FACE_OUTER_BOUND('',#3190,.T.);
#2160=FACE_OUTER_BOUND('',#3191,.T.);
#2161=FACE_OUTER_BOUND('',#3192,.T.);
#2162=FACE_OUTER_BOUND('',#3193,.T.);
#2163=FACE_OUTER_BOUND('',#3194,.T.);
#2164=FACE_OUTER_BOUND('',#3195,.T.);
#2165=FACE_OUTER_BOUND('',#3196,.T.);
#2166=FACE_OUTER_BOUND('',#3197,.T.);
#2167=FACE_OUTER_BOUND('',#3198,.T.);
#2168=FACE_OUTER_BOUND('',#3199,.T.);
#2169=FACE_OUTER_BOUND('',#3200,.T.);
#2170=FACE_OUTER_BOUND('',#3201,.T.);
#2171=FACE_OUTER_BOUND('',#3202,.T.);
#2172=FACE_OUTER_BOUND('',#3203,.T.);
#2173=FACE_OUTER_BOUND('',#3204,.T.);
#2174=FACE_OUTER_BOUND('',#3205,.T.);
#2175=FACE_OUTER_BOUND('',#3206,.T.);
#2176=FACE_OUTER_BOUND('',#3207,.T.);
#2177=FACE_OUTER_BOUND('',#3208,.T.);
#2178=FACE_OUTER_BOUND('',#3209,.T.);
#2179=FACE_OUTER_BOUND('',#3210,.T.);
#2180=FACE_OUTER_BOUND('',#3211,.T.);
#2181=FACE_OUTER_BOUND('',#3212,.T.);
#2182=FACE_OUTER_BOUND('',#3213,.T.);
#2183=FACE_OUTER_BOUND('',#3214,.T.);
#2184=FACE_OUTER_BOUND('',#3215,.T.);
#2185=FACE_OUTER_BOUND('',#3216,.T.);
#2186=FACE_OUTER_BOUND('',#3217,.T.);
#2187=FACE_OUTER_BOUND('',#3218,.T.);
#2188=FACE_OUTER_BOUND('',#3219,.T.);
#2189=FACE_OUTER_BOUND('',#3220,.T.);
#2190=FACE_OUTER_BOUND('',#3221,.T.);
#2191=FACE_OUTER_BOUND('',#3222,.T.);
#2192=FACE_OUTER_BOUND('',#3223,.T.);
#2193=FACE_OUTER_BOUND('',#3224,.T.);
#2194=FACE_OUTER_BOUND('',#3225,.T.);
#2195=FACE_OUTER_BOUND('',#3226,.T.);
#2196=FACE_OUTER_BOUND('',#3227,.T.);
#2197=FACE_OUTER_BOUND('',#3228,.T.);
#2198=FACE_OUTER_BOUND('',#3229,.T.);
#2199=FACE_OUTER_BOUND('',#3230,.T.);
#2200=FACE_OUTER_BOUND('',#3231,.T.);
#2201=FACE_OUTER_BOUND('',#3232,.T.);
#2202=FACE_OUTER_BOUND('',#3233,.T.);
#2203=FACE_OUTER_BOUND('',#3234,.T.);
#2204=FACE_OUTER_BOUND('',#3235,.T.);
#2205=FACE_OUTER_BOUND('',#3236,.T.);
#2206=FACE_OUTER_BOUND('',#3237,.T.);
#2207=FACE_OUTER_BOUND('',#3238,.T.);
#2208=FACE_OUTER_BOUND('',#3239,.T.);
#2209=FACE_OUTER_BOUND('',#3240,.T.);
#2210=FACE_OUTER_BOUND('',#3241,.T.);
#2211=FACE_OUTER_BOUND('',#3242,.T.);
#2212=FACE_OUTER_BOUND('',#3243,.T.);
#2213=FACE_OUTER_BOUND('',#3244,.T.);
#2214=FACE_OUTER_BOUND('',#3245,.T.);
#2215=FACE_OUTER_BOUND('',#3246,.T.);
#2216=FACE_OUTER_BOUND('',#3247,.T.);
#2217=FACE_OUTER_BOUND('',#3248,.T.);
#2218=FACE_OUTER_BOUND('',#3249,.T.);
#2219=FACE_OUTER_BOUND('',#3250,.T.);
#2220=FACE_OUTER_BOUND('',#3251,.T.);
#2221=FACE_OUTER_BOUND('',#3252,.T.);
#2222=FACE_OUTER_BOUND('',#3253,.T.);
#2223=FACE_OUTER_BOUND('',#3254,.T.);
#2224=FACE_OUTER_BOUND('',#3255,.T.);
#2225=FACE_OUTER_BOUND('',#3256,.T.);
#2226=FACE_OUTER_BOUND('',#3257,.T.);
#2227=FACE_OUTER_BOUND('',#3258,.T.);
#2228=FACE_OUTER_BOUND('',#3259,.T.);
#2229=FACE_OUTER_BOUND('',#3260,.T.);
#2230=FACE_OUTER_BOUND('',#3261,.T.);
#2231=FACE_OUTER_BOUND('',#3262,.T.);
#2232=FACE_OUTER_BOUND('',#3263,.T.);
#2233=FACE_OUTER_BOUND('',#3264,.T.);
#2234=FACE_OUTER_BOUND('',#3265,.T.);
#2235=FACE_OUTER_BOUND('',#3266,.T.);
#2236=FACE_OUTER_BOUND('',#3267,.T.);
#2237=FACE_OUTER_BOUND('',#3268,.T.);
#2238=FACE_OUTER_BOUND('',#3269,.T.);
#2239=FACE_OUTER_BOUND('',#3270,.T.);
#2240=FACE_OUTER_BOUND('',#3271,.T.);
#2241=FACE_OUTER_BOUND('',#3272,.T.);
#2242=FACE_OUTER_BOUND('',#3273,.T.);
#2243=FACE_OUTER_BOUND('',#3274,.T.);
#2244=FACE_OUTER_BOUND('',#3275,.T.);
#2245=FACE_OUTER_BOUND('',#3276,.T.);
#2246=FACE_OUTER_BOUND('',#3277,.T.);
#2247=FACE_OUTER_BOUND('',#3278,.T.);
#2248=FACE_OUTER_BOUND('',#3279,.T.);
#2249=FACE_OUTER_BOUND('',#3280,.T.);
#2250=FACE_OUTER_BOUND('',#3281,.T.);
#2251=FACE_OUTER_BOUND('',#3282,.T.);
#2252=FACE_OUTER_BOUND('',#3283,.T.);
#2253=FACE_OUTER_BOUND('',#3284,.T.);
#2254=FACE_OUTER_BOUND('',#3285,.T.);
#2255=FACE_OUTER_BOUND('',#3286,.T.);
#2256=FACE_OUTER_BOUND('',#3287,.T.);
#2257=FACE_OUTER_BOUND('',#3288,.T.);
#2258=FACE_OUTER_BOUND('',#3289,.T.);
#2259=FACE_OUTER_BOUND('',#3290,.T.);
#2260=FACE_OUTER_BOUND('',#3291,.T.);
#2261=FACE_OUTER_BOUND('',#3292,.T.);
#2262=FACE_OUTER_BOUND('',#3293,.T.);
#2263=FACE_OUTER_BOUND('',#3294,.T.);
#2264=FACE_OUTER_BOUND('',#3295,.T.);
#2265=FACE_OUTER_BOUND('',#3296,.T.);
#2266=FACE_OUTER_BOUND('',#3297,.T.);
#2267=FACE_OUTER_BOUND('',#3298,.T.);
#2268=FACE_OUTER_BOUND('',#3299,.T.);
#3138=EDGE_LOOP('',(#16287,#16288,#16289,#16290));
#3139=EDGE_LOOP('',(#16291,#16292,#16293,#16294));
#3140=EDGE_LOOP('',(#16295,#16296,#16297,#16298,#16299,#16300,#16301,#16302,
#16303,#16304,#16305,#16306,#16307,#16308,#16309,#16310,#16311,#16312,#16313,
#16314,#16315,#16316,#16317,#16318,#16319,#16320,#16321,#16322,#16323,#16324,
#16325,#16326,#16327,#16328,#16329,#16330,#16331,#16332,#16333,#16334,#16335,
#16336,#16337,#16338,#16339,#16340,#16341,#16342,#16343,#16344,#16345,#16346,
#16347,#16348,#16349,#16350,#16351,#16352,#16353,#16354,#16355,#16356,#16357,
#16358,#16359,#16360,#16361,#16362,#16363,#16364,#16365,#16366,#16367,#16368,
#16369,#16370,#16371,#16372,#16373,#16374,#16375,#16376,#16377,#16378,#16379,
#16380,#16381,#16382,#16383,#16384,#16385,#16386,#16387,#16388,#16389,#16390,
#16391,#16392,#16393,#16394,#16395,#16396,#16397,#16398,#16399,#16400,#16401,
#16402,#16403,#16404,#16405,#16406,#16407,#16408,#16409,#16410,#16411,#16412,
#16413,#16414,#16415,#16416,#16417,#16418,#16419,#16420,#16421,#16422,#16423,
#16424,#16425,#16426,#16427,#16428,#16429,#16430,#16431,#16432,#16433,#16434,
#16435,#16436,#16437,#16438,#16439,#16440,#16441,#16442,#16443,#16444));
#3141=EDGE_LOOP('',(#16445));
#3142=EDGE_LOOP('',(#16446));
#3143=EDGE_LOOP('',(#16447,#16448,#16449,#16450));
#3144=EDGE_LOOP('',(#16451,#16452,#16453,#16454,#16455,#16456,#16457,#16458,
#16459,#16460,#16461,#16462,#16463,#16464,#16465,#16466,#16467,#16468,#16469,
#16470,#16471,#16472,#16473,#16474,#16475,#16476,#16477,#16478,#16479,#16480,
#16481,#16482,#16483,#16484,#16485,#16486,#16487,#16488,#16489,#16490,#16491,
#16492,#16493,#16494,#16495,#16496,#16497,#16498,#16499,#16500,#16501,#16502,
#16503,#16504,#16505,#16506,#16507,#16508,#16509,#16510,#16511,#16512,#16513,
#16514,#16515,#16516,#16517,#16518,#16519,#16520,#16521,#16522,#16523,#16524,
#16525,#16526,#16527,#16528,#16529,#16530,#16531,#16532,#16533,#16534,#16535,
#16536,#16537,#16538,#16539,#16540,#16541,#16542,#16543,#16544,#16545,#16546,
#16547,#16548,#16549,#16550,#16551,#16552,#16553,#16554,#16555,#16556,#16557,
#16558,#16559,#16560,#16561,#16562,#16563,#16564,#16565,#16566,#16567,#16568,
#16569,#16570,#16571,#16572,#16573,#16574,#16575,#16576,#16577,#16578,#16579,
#16580,#16581,#16582,#16583,#16584,#16585,#16586,#16587,#16588,#16589,#16590,
#16591,#16592,#16593,#16594,#16595,#16596,#16597,#16598,#16599,#16600));
#3145=EDGE_LOOP('',(#16601));
#3146=EDGE_LOOP('',(#16602));
#3147=EDGE_LOOP('',(#16603,#16604,#16605,#16606));
#3148=EDGE_LOOP('',(#16607,#16608,#16609,#16610));
#3149=EDGE_LOOP('',(#16611,#16612,#16613,#16614));
#3150=EDGE_LOOP('',(#16615,#16616,#16617,#16618));
#3151=EDGE_LOOP('',(#16619,#16620,#16621,#16622));
#3152=EDGE_LOOP('',(#16623,#16624,#16625,#16626));
#3153=EDGE_LOOP('',(#16627,#16628,#16629,#16630));
#3154=EDGE_LOOP('',(#16631,#16632,#16633,#16634));
#3155=EDGE_LOOP('',(#16635,#16636,#16637,#16638));
#3156=EDGE_LOOP('',(#16639,#16640,#16641,#16642));
#3157=EDGE_LOOP('',(#16643,#16644,#16645,#16646));
#3158=EDGE_LOOP('',(#16647,#16648,#16649,#16650));
#3159=EDGE_LOOP('',(#16651,#16652,#16653,#16654));
#3160=EDGE_LOOP('',(#16655,#16656,#16657,#16658));
#3161=EDGE_LOOP('',(#16659,#16660,#16661,#16662));
#3162=EDGE_LOOP('',(#16663,#16664,#16665,#16666));
#3163=EDGE_LOOP('',(#16667,#16668,#16669,#16670));
#3164=EDGE_LOOP('',(#16671,#16672,#16673,#16674));
#3165=EDGE_LOOP('',(#16675,#16676,#16677,#16678));
#3166=EDGE_LOOP('',(#16679,#16680,#16681,#16682));
#3167=EDGE_LOOP('',(#16683,#16684,#16685,#16686));
#3168=EDGE_LOOP('',(#16687,#16688,#16689,#16690));
#3169=EDGE_LOOP('',(#16691,#16692,#16693,#16694));
#3170=EDGE_LOOP('',(#16695,#16696,#16697,#16698));
#3171=EDGE_LOOP('',(#16699,#16700,#16701,#16702));
#3172=EDGE_LOOP('',(#16703,#16704,#16705,#16706));
#3173=EDGE_LOOP('',(#16707,#16708,#16709,#16710));
#3174=EDGE_LOOP('',(#16711,#16712,#16713,#16714));
#3175=EDGE_LOOP('',(#16715,#16716,#16717,#16718));
#3176=EDGE_LOOP('',(#16719,#16720,#16721,#16722));
#3177=EDGE_LOOP('',(#16723,#16724,#16725,#16726));
#3178=EDGE_LOOP('',(#16727,#16728,#16729,#16730));
#3179=EDGE_LOOP('',(#16731,#16732,#16733,#16734));
#3180=EDGE_LOOP('',(#16735,#16736,#16737,#16738));
#3181=EDGE_LOOP('',(#16739,#16740,#16741,#16742));
#3182=EDGE_LOOP('',(#16743,#16744,#16745,#16746));
#3183=EDGE_LOOP('',(#16747,#16748,#16749,#16750));
#3184=EDGE_LOOP('',(#16751,#16752,#16753,#16754));
#3185=EDGE_LOOP('',(#16755,#16756,#16757,#16758));
#3186=EDGE_LOOP('',(#16759,#16760,#16761,#16762));
#3187=EDGE_LOOP('',(#16763,#16764,#16765,#16766));
#3188=EDGE_LOOP('',(#16767,#16768,#16769,#16770));
#3189=EDGE_LOOP('',(#16771,#16772,#16773,#16774));
#3190=EDGE_LOOP('',(#16775,#16776,#16777,#16778));
#3191=EDGE_LOOP('',(#16779,#16780,#16781,#16782));
#3192=EDGE_LOOP('',(#16783,#16784,#16785,#16786));
#3193=EDGE_LOOP('',(#16787,#16788,#16789,#16790));
#3194=EDGE_LOOP('',(#16791,#16792,#16793,#16794));
#3195=EDGE_LOOP('',(#16795,#16796,#16797,#16798));
#3196=EDGE_LOOP('',(#16799,#16800,#16801,#16802));
#3197=EDGE_LOOP('',(#16803,#16804,#16805,#16806));
#3198=EDGE_LOOP('',(#16807,#16808,#16809,#16810));
#3199=EDGE_LOOP('',(#16811,#16812,#16813,#16814));
#3200=EDGE_LOOP('',(#16815,#16816,#16817,#16818));
#3201=EDGE_LOOP('',(#16819,#16820,#16821,#16822));
#3202=EDGE_LOOP('',(#16823,#16824,#16825,#16826));
#3203=EDGE_LOOP('',(#16827,#16828,#16829,#16830));
#3204=EDGE_LOOP('',(#16831,#16832,#16833,#16834));
#3205=EDGE_LOOP('',(#16835,#16836,#16837,#16838));
#3206=EDGE_LOOP('',(#16839,#16840,#16841,#16842));
#3207=EDGE_LOOP('',(#16843,#16844,#16845,#16846));
#3208=EDGE_LOOP('',(#16847,#16848,#16849,#16850));
#3209=EDGE_LOOP('',(#16851,#16852,#16853,#16854));
#3210=EDGE_LOOP('',(#16855,#16856,#16857,#16858));
#3211=EDGE_LOOP('',(#16859,#16860,#16861,#16862));
#3212=EDGE_LOOP('',(#16863,#16864,#16865,#16866));
#3213=EDGE_LOOP('',(#16867,#16868,#16869,#16870));
#3214=EDGE_LOOP('',(#16871,#16872,#16873,#16874));
#3215=EDGE_LOOP('',(#16875,#16876,#16877,#16878));
#3216=EDGE_LOOP('',(#16879,#16880,#16881,#16882));
#3217=EDGE_LOOP('',(#16883,#16884,#16885,#16886));
#3218=EDGE_LOOP('',(#16887,#16888,#16889,#16890));
#3219=EDGE_LOOP('',(#16891,#16892,#16893,#16894));
#3220=EDGE_LOOP('',(#16895,#16896,#16897,#16898));
#3221=EDGE_LOOP('',(#16899,#16900,#16901,#16902));
#3222=EDGE_LOOP('',(#16903,#16904,#16905,#16906));
#3223=EDGE_LOOP('',(#16907,#16908,#16909,#16910));
#3224=EDGE_LOOP('',(#16911,#16912,#16913,#16914));
#3225=EDGE_LOOP('',(#16915,#16916,#16917,#16918));
#3226=EDGE_LOOP('',(#16919,#16920,#16921,#16922));
#3227=EDGE_LOOP('',(#16923,#16924,#16925,#16926));
#3228=EDGE_LOOP('',(#16927,#16928,#16929,#16930));
#3229=EDGE_LOOP('',(#16931,#16932,#16933,#16934));
#3230=EDGE_LOOP('',(#16935,#16936,#16937,#16938));
#3231=EDGE_LOOP('',(#16939,#16940,#16941,#16942));
#3232=EDGE_LOOP('',(#16943,#16944,#16945,#16946));
#3233=EDGE_LOOP('',(#16947,#16948,#16949,#16950));
#3234=EDGE_LOOP('',(#16951,#16952,#16953,#16954));
#3235=EDGE_LOOP('',(#16955,#16956,#16957,#16958));
#3236=EDGE_LOOP('',(#16959,#16960,#16961,#16962));
#3237=EDGE_LOOP('',(#16963,#16964,#16965,#16966));
#3238=EDGE_LOOP('',(#16967,#16968,#16969,#16970));
#3239=EDGE_LOOP('',(#16971,#16972,#16973,#16974));
#3240=EDGE_LOOP('',(#16975,#16976,#16977,#16978));
#3241=EDGE_LOOP('',(#16979,#16980,#16981,#16982));
#3242=EDGE_LOOP('',(#16983,#16984,#16985,#16986));
#3243=EDGE_LOOP('',(#16987,#16988,#16989,#16990));
#3244=EDGE_LOOP('',(#16991,#16992,#16993,#16994));
#3245=EDGE_LOOP('',(#16995,#16996,#16997,#16998));
#3246=EDGE_LOOP('',(#16999,#17000,#17001,#17002));
#3247=EDGE_LOOP('',(#17003,#17004,#17005,#17006));
#3248=EDGE_LOOP('',(#17007,#17008,#17009,#17010));
#3249=EDGE_LOOP('',(#17011,#17012,#17013,#17014));
#3250=EDGE_LOOP('',(#17015,#17016,#17017,#17018));
#3251=EDGE_LOOP('',(#17019,#17020,#17021,#17022));
#3252=EDGE_LOOP('',(#17023,#17024,#17025,#17026));
#3253=EDGE_LOOP('',(#17027,#17028,#17029,#17030));
#3254=EDGE_LOOP('',(#17031,#17032,#17033,#17034));
#3255=EDGE_LOOP('',(#17035,#17036,#17037,#17038));
#3256=EDGE_LOOP('',(#17039,#17040,#17041,#17042));
#3257=EDGE_LOOP('',(#17043,#17044,#17045,#17046));
#3258=EDGE_LOOP('',(#17047,#17048,#17049,#17050));
#3259=EDGE_LOOP('',(#17051,#17052,#17053,#17054));
#3260=EDGE_LOOP('',(#17055,#17056,#17057,#17058));
#3261=EDGE_LOOP('',(#17059,#17060,#17061,#17062));
#3262=EDGE_LOOP('',(#17063,#17064,#17065,#17066));
#3263=EDGE_LOOP('',(#17067,#17068,#17069,#17070));
#3264=EDGE_LOOP('',(#17071,#17072,#17073,#17074));
#3265=EDGE_LOOP('',(#17075,#17076,#17077,#17078));
#3266=EDGE_LOOP('',(#17079,#17080,#17081,#17082));
#3267=EDGE_LOOP('',(#17083,#17084,#17085,#17086));
#3268=EDGE_LOOP('',(#17087,#17088,#17089,#17090));
#3269=EDGE_LOOP('',(#17091,#17092,#17093,#17094));
#3270=EDGE_LOOP('',(#17095,#17096,#17097,#17098));
#3271=EDGE_LOOP('',(#17099,#17100,#17101,#17102));
#3272=EDGE_LOOP('',(#17103,#17104,#17105,#17106));
#3273=EDGE_LOOP('',(#17107,#17108,#17109,#17110));
#3274=EDGE_LOOP('',(#17111,#17112,#17113,#17114));
#3275=EDGE_LOOP('',(#17115,#17116,#17117,#17118));
#3276=EDGE_LOOP('',(#17119,#17120,#17121,#17122));
#3277=EDGE_LOOP('',(#17123,#17124,#17125,#17126));
#3278=EDGE_LOOP('',(#17127,#17128,#17129,#17130));
#3279=EDGE_LOOP('',(#17131,#17132,#17133,#17134));
#3280=EDGE_LOOP('',(#17135,#17136,#17137,#17138));
#3281=EDGE_LOOP('',(#17139,#17140,#17141,#17142));
#3282=EDGE_LOOP('',(#17143,#17144,#17145,#17146));
#3283=EDGE_LOOP('',(#17147,#17148,#17149,#17150));
#3284=EDGE_LOOP('',(#17151,#17152,#17153,#17154));
#3285=EDGE_LOOP('',(#17155,#17156,#17157,#17158));
#3286=EDGE_LOOP('',(#17159,#17160,#17161,#17162));
#3287=EDGE_LOOP('',(#17163,#17164,#17165,#17166));
#3288=EDGE_LOOP('',(#17167,#17168,#17169,#17170));
#3289=EDGE_LOOP('',(#17171,#17172,#17173,#17174));
#3290=EDGE_LOOP('',(#17175,#17176,#17177,#17178));
#3291=EDGE_LOOP('',(#17179,#17180,#17181,#17182));
#3292=EDGE_LOOP('',(#17183,#17184,#17185,#17186));
#3293=EDGE_LOOP('',(#17187,#17188,#17189,#17190));
#3294=EDGE_LOOP('',(#17191,#17192,#17193,#17194));
#3295=EDGE_LOOP('',(#17195,#17196,#17197,#17198));
#3296=EDGE_LOOP('',(#17199,#17200,#17201,#17202));
#3297=EDGE_LOOP('',(#17203,#17204,#17205,#17206));
#3298=EDGE_LOOP('',(#17207,#17208,#17209,#17210));
#3299=EDGE_LOOP('',(#17211,#17212,#17213,#17214));
#3697=CIRCLE('',#19499,0.750000000000001);
#3698=CIRCLE('',#19500,0.55);
#3699=CIRCLE('',#19502,0.55);
#3700=CIRCLE('',#19504,0.750000000000001);
#3701=CIRCLE('',#19506,0.750000000000001);
#3702=CIRCLE('',#19508,0.750000000000001);
#3703=CIRCLE('',#19510,0.55);
#3704=CIRCLE('',#19512,0.55);
#5456=LINE('',#59402,#6868);
#5457=LINE('',#59406,#6869);
#5458=LINE('',#59411,#6870);
#5459=LINE('',#59413,#6871);
#5460=LINE('',#59415,#6872);
#5461=LINE('',#59417,#6873);
#5462=LINE('',#59419,#6874);
#5463=LINE('',#59421,#6875);
#5464=LINE('',#59423,#6876);
#5465=LINE('',#59425,#6877);
#5466=LINE('',#59427,#6878);
#5467=LINE('',#59429,#6879);
#5468=LINE('',#59431,#6880);
#5469=LINE('',#59433,#6881);
#5470=LINE('',#59435,#6882);
#5471=LINE('',#59437,#6883);
#5472=LINE('',#59439,#6884);
#5473=LINE('',#59441,#6885);
#5474=LINE('',#59443,#6886);
#5475=LINE('',#59445,#6887);
#5476=LINE('',#59447,#6888);
#5477=LINE('',#59449,#6889);
#5478=LINE('',#59451,#6890);
#5479=LINE('',#59453,#6891);
#5480=LINE('',#59455,#6892);
#5481=LINE('',#59457,#6893);
#5482=LINE('',#59459,#6894);
#5483=LINE('',#59461,#6895);
#5484=LINE('',#59463,#6896);
#5485=LINE('',#59465,#6897);
#5486=LINE('',#59467,#6898);
#5487=LINE('',#59469,#6899);
#5488=LINE('',#59471,#6900);
#5489=LINE('',#59473,#6901);
#5490=LINE('',#59475,#6902);
#5491=LINE('',#59477,#6903);
#5492=LINE('',#59479,#6904);
#5493=LINE('',#59481,#6905);
#5494=LINE('',#59483,#6906);
#5495=LINE('',#59485,#6907);
#5496=LINE('',#59487,#6908);
#5497=LINE('',#59489,#6909);
#5498=LINE('',#59491,#6910);
#5499=LINE('',#59493,#6911);
#5500=LINE('',#59495,#6912);
#5501=LINE('',#59497,#6913);
#5502=LINE('',#59499,#6914);
#5503=LINE('',#59501,#6915);
#5504=LINE('',#59503,#6916);
#5505=LINE('',#59505,#6917);
#5506=LINE('',#59507,#6918);
#5507=LINE('',#59509,#6919);
#5508=LINE('',#59511,#6920);
#5509=LINE('',#59513,#6921);
#5510=LINE('',#59515,#6922);
#5511=LINE('',#59517,#6923);
#5512=LINE('',#59519,#6924);
#5513=LINE('',#59521,#6925);
#5514=LINE('',#59523,#6926);
#5515=LINE('',#59525,#6927);
#5516=LINE('',#59527,#6928);
#5517=LINE('',#59529,#6929);
#5518=LINE('',#59531,#6930);
#5519=LINE('',#59533,#6931);
#5520=LINE('',#59535,#6932);
#5521=LINE('',#59537,#6933);
#5522=LINE('',#59539,#6934);
#5523=LINE('',#59541,#6935);
#5524=LINE('',#59543,#6936);
#5525=LINE('',#59545,#6937);
#5526=LINE('',#59547,#6938);
#5527=LINE('',#59549,#6939);
#5528=LINE('',#59551,#6940);
#5529=LINE('',#59553,#6941);
#5530=LINE('',#59555,#6942);
#5531=LINE('',#59557,#6943);
#5532=LINE('',#59559,#6944);
#5533=LINE('',#59561,#6945);
#5534=LINE('',#59563,#6946);
#5535=LINE('',#59565,#6947);
#5536=LINE('',#59567,#6948);
#5537=LINE('',#59569,#6949);
#5538=LINE('',#59571,#6950);
#5539=LINE('',#59573,#6951);
#5540=LINE('',#59575,#6952);
#5541=LINE('',#59577,#6953);
#5542=LINE('',#59579,#6954);
#5543=LINE('',#59581,#6955);
#5544=LINE('',#59583,#6956);
#5545=LINE('',#59585,#6957);
#5546=LINE('',#59587,#6958);
#5547=LINE('',#59589,#6959);
#5548=LINE('',#59591,#6960);
#5549=LINE('',#59593,#6961);
#5550=LINE('',#59595,#6962);
#5551=LINE('',#59597,#6963);
#5552=LINE('',#59599,#6964);
#5553=LINE('',#59601,#6965);
#5554=LINE('',#59603,#6966);
#5555=LINE('',#59605,#6967);
#5556=LINE('',#59607,#6968);
#5557=LINE('',#59609,#6969);
#5558=LINE('',#59611,#6970);
#5559=LINE('',#59613,#6971);
#5560=LINE('',#59615,#6972);
#5561=LINE('',#59617,#6973);
#5562=LINE('',#59619,#6974);
#5563=LINE('',#59621,#6975);
#5564=LINE('',#59623,#6976);
#5565=LINE('',#59625,#6977);
#5566=LINE('',#59627,#6978);
#5567=LINE('',#59629,#6979);
#5568=LINE('',#59631,#6980);
#5569=LINE('',#59633,#6981);
#5570=LINE('',#59635,#6982);
#5571=LINE('',#59637,#6983);
#5572=LINE('',#59639,#6984);
#5573=LINE('',#59641,#6985);
#5574=LINE('',#59643,#6986);
#5575=LINE('',#59645,#6987);
#5576=LINE('',#59647,#6988);
#5577=LINE('',#59649,#6989);
#5578=LINE('',#59651,#6990);
#5579=LINE('',#59653,#6991);
#5580=LINE('',#59655,#6992);
#5581=LINE('',#59657,#6993);
#5582=LINE('',#59659,#6994);
#5583=LINE('',#59661,#6995);
#5584=LINE('',#59663,#6996);
#5585=LINE('',#59665,#6997);
#5586=LINE('',#59667,#6998);
#5587=LINE('',#59669,#6999);
#5588=LINE('',#59671,#7000);
#5589=LINE('',#59673,#7001);
#5590=LINE('',#59675,#7002);
#5591=LINE('',#59677,#7003);
#5592=LINE('',#59679,#7004);
#5593=LINE('',#59681,#7005);
#5594=LINE('',#59683,#7006);
#5595=LINE('',#59685,#7007);
#5596=LINE('',#59687,#7008);
#5597=LINE('',#59689,#7009);
#5598=LINE('',#59691,#7010);
#5599=LINE('',#59693,#7011);
#5600=LINE('',#59695,#7012);
#5601=LINE('',#59697,#7013);
#5602=LINE('',#59699,#7014);
#5603=LINE('',#59701,#7015);
#5604=LINE('',#59703,#7016);
#5605=LINE('',#59705,#7017);
#5606=LINE('',#59707,#7018);
#5607=LINE('',#59708,#7019);
#5608=LINE('',#59714,#7020);
#5609=LINE('',#59718,#7021);
#5610=LINE('',#59720,#7022);
#5611=LINE('',#59722,#7023);
#5612=LINE('',#59724,#7024);
#5613=LINE('',#59726,#7025);
#5614=LINE('',#59728,#7026);
#5615=LINE('',#59730,#7027);
#5616=LINE('',#59732,#7028);
#5617=LINE('',#59734,#7029);
#5618=LINE('',#59736,#7030);
#5619=LINE('',#59738,#7031);
#5620=LINE('',#59740,#7032);
#5621=LINE('',#59742,#7033);
#5622=LINE('',#59744,#7034);
#5623=LINE('',#59746,#7035);
#5624=LINE('',#59748,#7036);
#5625=LINE('',#59750,#7037);
#5626=LINE('',#59752,#7038);
#5627=LINE('',#59754,#7039);
#5628=LINE('',#59756,#7040);
#5629=LINE('',#59758,#7041);
#5630=LINE('',#59760,#7042);
#5631=LINE('',#59762,#7043);
#5632=LINE('',#59764,#7044);
#5633=LINE('',#59766,#7045);
#5634=LINE('',#59768,#7046);
#5635=LINE('',#59770,#7047);
#5636=LINE('',#59772,#7048);
#5637=LINE('',#59774,#7049);
#5638=LINE('',#59776,#7050);
#5639=LINE('',#59778,#7051);
#5640=LINE('',#59780,#7052);
#5641=LINE('',#59782,#7053);
#5642=LINE('',#59784,#7054);
#5643=LINE('',#59786,#7055);
#5644=LINE('',#59788,#7056);
#5645=LINE('',#59790,#7057);
#5646=LINE('',#59792,#7058);
#5647=LINE('',#59794,#7059);
#5648=LINE('',#59796,#7060);
#5649=LINE('',#59798,#7061);
#5650=LINE('',#59800,#7062);
#5651=LINE('',#59802,#7063);
#5652=LINE('',#59804,#7064);
#5653=LINE('',#59806,#7065);
#5654=LINE('',#59808,#7066);
#5655=LINE('',#59810,#7067);
#5656=LINE('',#59812,#7068);
#5657=LINE('',#59814,#7069);
#5658=LINE('',#59816,#7070);
#5659=LINE('',#59818,#7071);
#5660=LINE('',#59820,#7072);
#5661=LINE('',#59822,#7073);
#5662=LINE('',#59824,#7074);
#5663=LINE('',#59826,#7075);
#5664=LINE('',#59828,#7076);
#5665=LINE('',#59830,#7077);
#5666=LINE('',#59832,#7078);
#5667=LINE('',#59834,#7079);
#5668=LINE('',#59836,#7080);
#5669=LINE('',#59838,#7081);
#5670=LINE('',#59840,#7082);
#5671=LINE('',#59842,#7083);
#5672=LINE('',#59844,#7084);
#5673=LINE('',#59846,#7085);
#5674=LINE('',#59848,#7086);
#5675=LINE('',#59850,#7087);
#5676=LINE('',#59852,#7088);
#5677=LINE('',#59854,#7089);
#5678=LINE('',#59856,#7090);
#5679=LINE('',#59858,#7091);
#5680=LINE('',#59860,#7092);
#5681=LINE('',#59862,#7093);
#5682=LINE('',#59864,#7094);
#5683=LINE('',#59866,#7095);
#5684=LINE('',#59868,#7096);
#5685=LINE('',#59870,#7097);
#5686=LINE('',#59872,#7098);
#5687=LINE('',#59874,#7099);
#5688=LINE('',#59876,#7100);
#5689=LINE('',#59878,#7101);
#5690=LINE('',#59880,#7102);
#5691=LINE('',#59882,#7103);
#5692=LINE('',#59884,#7104);
#5693=LINE('',#59886,#7105);
#5694=LINE('',#59888,#7106);
#5695=LINE('',#59890,#7107);
#5696=LINE('',#59892,#7108);
#5697=LINE('',#59894,#7109);
#5698=LINE('',#59896,#7110);
#5699=LINE('',#59898,#7111);
#5700=LINE('',#59900,#7112);
#5701=LINE('',#59902,#7113);
#5702=LINE('',#59904,#7114);
#5703=LINE('',#59906,#7115);
#5704=LINE('',#59908,#7116);
#5705=LINE('',#59910,#7117);
#5706=LINE('',#59912,#7118);
#5707=LINE('',#59914,#7119);
#5708=LINE('',#59916,#7120);
#5709=LINE('',#59918,#7121);
#5710=LINE('',#59920,#7122);
#5711=LINE('',#59922,#7123);
#5712=LINE('',#59924,#7124);
#5713=LINE('',#59926,#7125);
#5714=LINE('',#59928,#7126);
#5715=LINE('',#59930,#7127);
#5716=LINE('',#59932,#7128);
#5717=LINE('',#59934,#7129);
#5718=LINE('',#59936,#7130);
#5719=LINE('',#59938,#7131);
#5720=LINE('',#59940,#7132);
#5721=LINE('',#59942,#7133);
#5722=LINE('',#59944,#7134);
#5723=LINE('',#59946,#7135);
#5724=LINE('',#59948,#7136);
#5725=LINE('',#59950,#7137);
#5726=LINE('',#59952,#7138);
#5727=LINE('',#59954,#7139);
#5728=LINE('',#59956,#7140);
#5729=LINE('',#59958,#7141);
#5730=LINE('',#59960,#7142);
#5731=LINE('',#59962,#7143);
#5732=LINE('',#59964,#7144);
#5733=LINE('',#59966,#7145);
#5734=LINE('',#59968,#7146);
#5735=LINE('',#59970,#7147);
#5736=LINE('',#59972,#7148);
#5737=LINE('',#59974,#7149);
#5738=LINE('',#59976,#7150);
#5739=LINE('',#59978,#7151);
#5740=LINE('',#59980,#7152);
#5741=LINE('',#59982,#7153);
#5742=LINE('',#59984,#7154);
#5743=LINE('',#59986,#7155);
#5744=LINE('',#59988,#7156);
#5745=LINE('',#59990,#7157);
#5746=LINE('',#59992,#7158);
#5747=LINE('',#59994,#7159);
#5748=LINE('',#59996,#7160);
#5749=LINE('',#59998,#7161);
#5750=LINE('',#60000,#7162);
#5751=LINE('',#60002,#7163);
#5752=LINE('',#60004,#7164);
#5753=LINE('',#60006,#7165);
#5754=LINE('',#60008,#7166);
#5755=LINE('',#60010,#7167);
#5756=LINE('',#60012,#7168);
#5757=LINE('',#60014,#7169);
#5758=LINE('',#60015,#7170);
#5759=LINE('',#60020,#7171);
#5760=LINE('',#60024,#7172);
#5761=LINE('',#60027,#7173);
#5762=LINE('',#60029,#7174);
#5763=LINE('',#60030,#7175);
#5764=LINE('',#60032,#7176);
#5765=LINE('',#60034,#7177);
#5766=LINE('',#60036,#7178);
#5767=LINE('',#60038,#7179);
#5768=LINE('',#60040,#7180);
#5769=LINE('',#60042,#7181);
#5770=LINE('',#60044,#7182);
#5771=LINE('',#60046,#7183);
#5772=LINE('',#60048,#7184);
#5773=LINE('',#60050,#7185);
#5774=LINE('',#60052,#7186);
#5775=LINE('',#60054,#7187);
#5776=LINE('',#60056,#7188);
#5777=LINE('',#60058,#7189);
#5778=LINE('',#60060,#7190);
#5779=LINE('',#60062,#7191);
#5780=LINE('',#60064,#7192);
#5781=LINE('',#60066,#7193);
#5782=LINE('',#60068,#7194);
#5783=LINE('',#60070,#7195);
#5784=LINE('',#60072,#7196);
#5785=LINE('',#60074,#7197);
#5786=LINE('',#60076,#7198);
#5787=LINE('',#60078,#7199);
#5788=LINE('',#60080,#7200);
#5789=LINE('',#60082,#7201);
#5790=LINE('',#60084,#7202);
#5791=LINE('',#60086,#7203);
#5792=LINE('',#60088,#7204);
#5793=LINE('',#60090,#7205);
#5794=LINE('',#60092,#7206);
#5795=LINE('',#60094,#7207);
#5796=LINE('',#60096,#7208);
#5797=LINE('',#60098,#7209);
#5798=LINE('',#60100,#7210);
#5799=LINE('',#60102,#7211);
#5800=LINE('',#60104,#7212);
#5801=LINE('',#60106,#7213);
#5802=LINE('',#60108,#7214);
#5803=LINE('',#60110,#7215);
#5804=LINE('',#60112,#7216);
#5805=LINE('',#60114,#7217);
#5806=LINE('',#60116,#7218);
#5807=LINE('',#60118,#7219);
#5808=LINE('',#60120,#7220);
#5809=LINE('',#60122,#7221);
#5810=LINE('',#60124,#7222);
#5811=LINE('',#60126,#7223);
#5812=LINE('',#60128,#7224);
#5813=LINE('',#60130,#7225);
#5814=LINE('',#60132,#7226);
#5815=LINE('',#60134,#7227);
#5816=LINE('',#60136,#7228);
#5817=LINE('',#60138,#7229);
#5818=LINE('',#60140,#7230);
#5819=LINE('',#60142,#7231);
#5820=LINE('',#60144,#7232);
#5821=LINE('',#60146,#7233);
#5822=LINE('',#60148,#7234);
#5823=LINE('',#60150,#7235);
#5824=LINE('',#60152,#7236);
#5825=LINE('',#60154,#7237);
#5826=LINE('',#60156,#7238);
#5827=LINE('',#60158,#7239);
#5828=LINE('',#60160,#7240);
#5829=LINE('',#60162,#7241);
#5830=LINE('',#60164,#7242);
#5831=LINE('',#60166,#7243);
#5832=LINE('',#60168,#7244);
#5833=LINE('',#60170,#7245);
#5834=LINE('',#60172,#7246);
#5835=LINE('',#60174,#7247);
#5836=LINE('',#60176,#7248);
#5837=LINE('',#60178,#7249);
#5838=LINE('',#60180,#7250);
#5839=LINE('',#60182,#7251);
#5840=LINE('',#60184,#7252);
#5841=LINE('',#60186,#7253);
#5842=LINE('',#60188,#7254);
#5843=LINE('',#60190,#7255);
#5844=LINE('',#60192,#7256);
#5845=LINE('',#60194,#7257);
#5846=LINE('',#60196,#7258);
#5847=LINE('',#60198,#7259);
#5848=LINE('',#60200,#7260);
#5849=LINE('',#60202,#7261);
#5850=LINE('',#60204,#7262);
#5851=LINE('',#60206,#7263);
#5852=LINE('',#60208,#7264);
#5853=LINE('',#60210,#7265);
#5854=LINE('',#60212,#7266);
#5855=LINE('',#60214,#7267);
#5856=LINE('',#60216,#7268);
#5857=LINE('',#60218,#7269);
#5858=LINE('',#60220,#7270);
#5859=LINE('',#60222,#7271);
#5860=LINE('',#60224,#7272);
#5861=LINE('',#60226,#7273);
#5862=LINE('',#60228,#7274);
#5863=LINE('',#60230,#7275);
#5864=LINE('',#60232,#7276);
#5865=LINE('',#60234,#7277);
#5866=LINE('',#60236,#7278);
#5867=LINE('',#60238,#7279);
#5868=LINE('',#60240,#7280);
#5869=LINE('',#60242,#7281);
#5870=LINE('',#60244,#7282);
#5871=LINE('',#60246,#7283);
#5872=LINE('',#60248,#7284);
#5873=LINE('',#60250,#7285);
#5874=LINE('',#60252,#7286);
#5875=LINE('',#60254,#7287);
#5876=LINE('',#60256,#7288);
#5877=LINE('',#60258,#7289);
#5878=LINE('',#60260,#7290);
#5879=LINE('',#60262,#7291);
#5880=LINE('',#60264,#7292);
#5881=LINE('',#60266,#7293);
#5882=LINE('',#60268,#7294);
#5883=LINE('',#60270,#7295);
#5884=LINE('',#60272,#7296);
#5885=LINE('',#60274,#7297);
#5886=LINE('',#60276,#7298);
#5887=LINE('',#60278,#7299);
#5888=LINE('',#60280,#7300);
#5889=LINE('',#60282,#7301);
#5890=LINE('',#60284,#7302);
#5891=LINE('',#60286,#7303);
#5892=LINE('',#60288,#7304);
#5893=LINE('',#60290,#7305);
#5894=LINE('',#60292,#7306);
#5895=LINE('',#60294,#7307);
#5896=LINE('',#60296,#7308);
#5897=LINE('',#60298,#7309);
#5898=LINE('',#60300,#7310);
#5899=LINE('',#60302,#7311);
#5900=LINE('',#60304,#7312);
#5901=LINE('',#60306,#7313);
#5902=LINE('',#60308,#7314);
#5903=LINE('',#60310,#7315);
#5904=LINE('',#60312,#7316);
#5905=LINE('',#60314,#7317);
#5906=LINE('',#60316,#7318);
#5907=LINE('',#60318,#7319);
#5908=LINE('',#60320,#7320);
#5909=LINE('',#60322,#7321);
#5910=LINE('',#60324,#7322);
#5911=LINE('',#60326,#7323);
#6868=VECTOR('',#22798,0.650000000000001);
#6869=VECTOR('',#22803,0.55);
#6870=VECTOR('',#22808,10.);
#6871=VECTOR('',#22809,10.);
#6872=VECTOR('',#22810,10.);
#6873=VECTOR('',#22811,10.);
#6874=VECTOR('',#22812,10.);
#6875=VECTOR('',#22813,10.);
#6876=VECTOR('',#22814,10.);
#6877=VECTOR('',#22815,10.);
#6878=VECTOR('',#22816,10.);
#6879=VECTOR('',#22817,10.);
#6880=VECTOR('',#22818,10.);
#6881=VECTOR('',#22819,10.);
#6882=VECTOR('',#22820,10.);
#6883=VECTOR('',#22821,10.);
#6884=VECTOR('',#22822,10.);
#6885=VECTOR('',#22823,10.);
#6886=VECTOR('',#22824,10.);
#6887=VECTOR('',#22825,10.);
#6888=VECTOR('',#22826,10.);
#6889=VECTOR('',#22827,10.);
#6890=VECTOR('',#22828,10.);
#6891=VECTOR('',#22829,10.);
#6892=VECTOR('',#22830,10.);
#6893=VECTOR('',#22831,10.);
#6894=VECTOR('',#22832,10.);
#6895=VECTOR('',#22833,10.);
#6896=VECTOR('',#22834,10.);
#6897=VECTOR('',#22835,10.);
#6898=VECTOR('',#22836,10.);
#6899=VECTOR('',#22837,10.);
#6900=VECTOR('',#22838,10.);
#6901=VECTOR('',#22839,10.);
#6902=VECTOR('',#22840,10.);
#6903=VECTOR('',#22841,10.);
#6904=VECTOR('',#22842,10.);
#6905=VECTOR('',#22843,10.);
#6906=VECTOR('',#22844,10.);
#6907=VECTOR('',#22845,10.);
#6908=VECTOR('',#22846,10.);
#6909=VECTOR('',#22847,10.);
#6910=VECTOR('',#22848,10.);
#6911=VECTOR('',#22849,10.);
#6912=VECTOR('',#22850,10.);
#6913=VECTOR('',#22851,10.);
#6914=VECTOR('',#22852,10.);
#6915=VECTOR('',#22853,10.);
#6916=VECTOR('',#22854,10.);
#6917=VECTOR('',#22855,10.);
#6918=VECTOR('',#22856,10.);
#6919=VECTOR('',#22857,10.);
#6920=VECTOR('',#22858,10.);
#6921=VECTOR('',#22859,10.);
#6922=VECTOR('',#22860,10.);
#6923=VECTOR('',#22861,10.);
#6924=VECTOR('',#22862,10.);
#6925=VECTOR('',#22863,10.);
#6926=VECTOR('',#22864,10.);
#6927=VECTOR('',#22865,10.);
#6928=VECTOR('',#22866,10.);
#6929=VECTOR('',#22867,10.);
#6930=VECTOR('',#22868,10.);
#6931=VECTOR('',#22869,10.);
#6932=VECTOR('',#22870,10.);
#6933=VECTOR('',#22871,10.);
#6934=VECTOR('',#22872,10.);
#6935=VECTOR('',#22873,10.);
#6936=VECTOR('',#22874,10.);
#6937=VECTOR('',#22875,10.);
#6938=VECTOR('',#22876,10.);
#6939=VECTOR('',#22877,10.);
#6940=VECTOR('',#22878,10.);
#6941=VECTOR('',#22879,10.);
#6942=VECTOR('',#22880,10.);
#6943=VECTOR('',#22881,10.);
#6944=VECTOR('',#22882,10.);
#6945=VECTOR('',#22883,10.);
#6946=VECTOR('',#22884,10.);
#6947=VECTOR('',#22885,10.);
#6948=VECTOR('',#22886,10.);
#6949=VECTOR('',#22887,10.);
#6950=VECTOR('',#22888,10.);
#6951=VECTOR('',#22889,10.);
#6952=VECTOR('',#22890,10.);
#6953=VECTOR('',#22891,10.);
#6954=VECTOR('',#22892,10.);
#6955=VECTOR('',#22893,10.);
#6956=VECTOR('',#22894,10.);
#6957=VECTOR('',#22895,10.);
#6958=VECTOR('',#22896,10.);
#6959=VECTOR('',#22897,10.);
#6960=VECTOR('',#22898,10.);
#6961=VECTOR('',#22899,10.);
#6962=VECTOR('',#22900,10.);
#6963=VECTOR('',#22901,10.);
#6964=VECTOR('',#22902,10.);
#6965=VECTOR('',#22903,10.);
#6966=VECTOR('',#22904,10.);
#6967=VECTOR('',#22905,10.);
#6968=VECTOR('',#22906,10.);
#6969=VECTOR('',#22907,10.);
#6970=VECTOR('',#22908,10.);
#6971=VECTOR('',#22909,10.);
#6972=VECTOR('',#22910,10.);
#6973=VECTOR('',#22911,10.);
#6974=VECTOR('',#22912,10.);
#6975=VECTOR('',#22913,10.);
#6976=VECTOR('',#22914,10.);
#6977=VECTOR('',#22915,10.);
#6978=VECTOR('',#22916,10.);
#6979=VECTOR('',#22917,10.);
#6980=VECTOR('',#22918,10.);
#6981=VECTOR('',#22919,10.);
#6982=VECTOR('',#22920,10.);
#6983=VECTOR('',#22921,10.);
#6984=VECTOR('',#22922,10.);
#6985=VECTOR('',#22923,10.);
#6986=VECTOR('',#22924,10.);
#6987=VECTOR('',#22925,10.);
#6988=VECTOR('',#22926,10.);
#6989=VECTOR('',#22927,10.);
#6990=VECTOR('',#22928,10.);
#6991=VECTOR('',#22929,10.);
#6992=VECTOR('',#22930,10.);
#6993=VECTOR('',#22931,10.);
#6994=VECTOR('',#22932,10.);
#6995=VECTOR('',#22933,10.);
#6996=VECTOR('',#22934,10.);
#6997=VECTOR('',#22935,10.);
#6998=VECTOR('',#22936,10.);
#6999=VECTOR('',#22937,10.);
#7000=VECTOR('',#22938,10.);
#7001=VECTOR('',#22939,10.);
#7002=VECTOR('',#22940,10.);
#7003=VECTOR('',#22941,10.);
#7004=VECTOR('',#22942,10.);
#7005=VECTOR('',#22943,10.);
#7006=VECTOR('',#22944,10.);
#7007=VECTOR('',#22945,10.);
#7008=VECTOR('',#22946,10.);
#7009=VECTOR('',#22947,10.);
#7010=VECTOR('',#22948,10.);
#7011=VECTOR('',#22949,10.);
#7012=VECTOR('',#22950,10.);
#7013=VECTOR('',#22951,10.);
#7014=VECTOR('',#22952,10.);
#7015=VECTOR('',#22953,10.);
#7016=VECTOR('',#22954,10.);
#7017=VECTOR('',#22955,10.);
#7018=VECTOR('',#22956,10.);
#7019=VECTOR('',#22957,10.);
#7020=VECTOR('',#22964,0.650000000000001);
#7021=VECTOR('',#22967,10.);
#7022=VECTOR('',#22968,10.);
#7023=VECTOR('',#22969,10.);
#7024=VECTOR('',#22970,10.);
#7025=VECTOR('',#22971,10.);
#7026=VECTOR('',#22972,10.);
#7027=VECTOR('',#22973,10.);
#7028=VECTOR('',#22974,10.);
#7029=VECTOR('',#22975,10.);
#7030=VECTOR('',#22976,10.);
#7031=VECTOR('',#22977,10.);
#7032=VECTOR('',#22978,10.);
#7033=VECTOR('',#22979,10.);
#7034=VECTOR('',#22980,10.);
#7035=VECTOR('',#22981,10.);
#7036=VECTOR('',#22982,10.);
#7037=VECTOR('',#22983,10.);
#7038=VECTOR('',#22984,10.);
#7039=VECTOR('',#22985,10.);
#7040=VECTOR('',#22986,10.);
#7041=VECTOR('',#22987,10.);
#7042=VECTOR('',#22988,10.);
#7043=VECTOR('',#22989,10.);
#7044=VECTOR('',#22990,10.);
#7045=VECTOR('',#22991,10.);
#7046=VECTOR('',#22992,10.);
#7047=VECTOR('',#22993,10.);
#7048=VECTOR('',#22994,10.);
#7049=VECTOR('',#22995,10.);
#7050=VECTOR('',#22996,10.);
#7051=VECTOR('',#22997,10.);
#7052=VECTOR('',#22998,10.);
#7053=VECTOR('',#22999,10.);
#7054=VECTOR('',#23000,10.);
#7055=VECTOR('',#23001,10.);
#7056=VECTOR('',#23002,10.);
#7057=VECTOR('',#23003,10.);
#7058=VECTOR('',#23004,10.);
#7059=VECTOR('',#23005,10.);
#7060=VECTOR('',#23006,10.);
#7061=VECTOR('',#23007,10.);
#7062=VECTOR('',#23008,10.);
#7063=VECTOR('',#23009,10.);
#7064=VECTOR('',#23010,10.);
#7065=VECTOR('',#23011,10.);
#7066=VECTOR('',#23012,10.);
#7067=VECTOR('',#23013,10.);
#7068=VECTOR('',#23014,10.);
#7069=VECTOR('',#23015,10.);
#7070=VECTOR('',#23016,10.);
#7071=VECTOR('',#23017,10.);
#7072=VECTOR('',#23018,10.);
#7073=VECTOR('',#23019,10.);
#7074=VECTOR('',#23020,10.);
#7075=VECTOR('',#23021,10.);
#7076=VECTOR('',#23022,10.);
#7077=VECTOR('',#23023,10.);
#7078=VECTOR('',#23024,10.);
#7079=VECTOR('',#23025,10.);
#7080=VECTOR('',#23026,10.);
#7081=VECTOR('',#23027,10.);
#7082=VECTOR('',#23028,10.);
#7083=VECTOR('',#23029,10.);
#7084=VECTOR('',#23030,10.);
#7085=VECTOR('',#23031,10.);
#7086=VECTOR('',#23032,10.);
#7087=VECTOR('',#23033,10.);
#7088=VECTOR('',#23034,10.);
#7089=VECTOR('',#23035,10.);
#7090=VECTOR('',#23036,10.);
#7091=VECTOR('',#23037,10.);
#7092=VECTOR('',#23038,10.);
#7093=VECTOR('',#23039,10.);
#7094=VECTOR('',#23040,10.);
#7095=VECTOR('',#23041,10.);
#7096=VECTOR('',#23042,10.);
#7097=VECTOR('',#23043,10.);
#7098=VECTOR('',#23044,10.);
#7099=VECTOR('',#23045,10.);
#7100=VECTOR('',#23046,10.);
#7101=VECTOR('',#23047,10.);
#7102=VECTOR('',#23048,10.);
#7103=VECTOR('',#23049,10.);
#7104=VECTOR('',#23050,10.);
#7105=VECTOR('',#23051,10.);
#7106=VECTOR('',#23052,10.);
#7107=VECTOR('',#23053,10.);
#7108=VECTOR('',#23054,10.);
#7109=VECTOR('',#23055,10.);
#7110=VECTOR('',#23056,10.);
#7111=VECTOR('',#23057,10.);
#7112=VECTOR('',#23058,10.);
#7113=VECTOR('',#23059,10.);
#7114=VECTOR('',#23060,10.);
#7115=VECTOR('',#23061,10.);
#7116=VECTOR('',#23062,10.);
#7117=VECTOR('',#23063,10.);
#7118=VECTOR('',#23064,10.);
#7119=VECTOR('',#23065,10.);
#7120=VECTOR('',#23066,10.);
#7121=VECTOR('',#23067,10.);
#7122=VECTOR('',#23068,10.);
#7123=VECTOR('',#23069,10.);
#7124=VECTOR('',#23070,10.);
#7125=VECTOR('',#23071,10.);
#7126=VECTOR('',#23072,10.);
#7127=VECTOR('',#23073,10.);
#7128=VECTOR('',#23074,10.);
#7129=VECTOR('',#23075,10.);
#7130=VECTOR('',#23076,10.);
#7131=VECTOR('',#23077,10.);
#7132=VECTOR('',#23078,10.);
#7133=VECTOR('',#23079,10.);
#7134=VECTOR('',#23080,10.);
#7135=VECTOR('',#23081,10.);
#7136=VECTOR('',#23082,10.);
#7137=VECTOR('',#23083,10.);
#7138=VECTOR('',#23084,10.);
#7139=VECTOR('',#23085,10.);
#7140=VECTOR('',#23086,10.);
#7141=VECTOR('',#23087,10.);
#7142=VECTOR('',#23088,10.);
#7143=VECTOR('',#23089,10.);
#7144=VECTOR('',#23090,10.);
#7145=VECTOR('',#23091,10.);
#7146=VECTOR('',#23092,10.);
#7147=VECTOR('',#23093,10.);
#7148=VECTOR('',#23094,10.);
#7149=VECTOR('',#23095,10.);
#7150=VECTOR('',#23096,10.);
#7151=VECTOR('',#23097,10.);
#7152=VECTOR('',#23098,10.);
#7153=VECTOR('',#23099,10.);
#7154=VECTOR('',#23100,10.);
#7155=VECTOR('',#23101,10.);
#7156=VECTOR('',#23102,10.);
#7157=VECTOR('',#23103,10.);
#7158=VECTOR('',#23104,10.);
#7159=VECTOR('',#23105,10.);
#7160=VECTOR('',#23106,10.);
#7161=VECTOR('',#23107,10.);
#7162=VECTOR('',#23108,10.);
#7163=VECTOR('',#23109,10.);
#7164=VECTOR('',#23110,10.);
#7165=VECTOR('',#23111,10.);
#7166=VECTOR('',#23112,10.);
#7167=VECTOR('',#23113,10.);
#7168=VECTOR('',#23114,10.);
#7169=VECTOR('',#23115,10.);
#7170=VECTOR('',#23116,10.);
#7171=VECTOR('',#23121,0.650000000000001);
#7172=VECTOR('',#23126,0.55);
#7173=VECTOR('',#23131,0.650000000000001);
#7174=VECTOR('',#23134,10.);
#7175=VECTOR('',#23135,10.);
#7176=VECTOR('',#23138,10.);
#7177=VECTOR('',#23141,10.);
#7178=VECTOR('',#23144,10.);
#7179=VECTOR('',#23147,10.);
#7180=VECTOR('',#23150,10.);
#7181=VECTOR('',#23153,10.);
#7182=VECTOR('',#23156,10.);
#7183=VECTOR('',#23159,10.);
#7184=VECTOR('',#23162,10.);
#7185=VECTOR('',#23165,10.);
#7186=VECTOR('',#23168,10.);
#7187=VECTOR('',#23171,10.);
#7188=VECTOR('',#23174,10.);
#7189=VECTOR('',#23177,10.);
#7190=VECTOR('',#23180,10.);
#7191=VECTOR('',#23183,10.);
#7192=VECTOR('',#23186,10.);
#7193=VECTOR('',#23189,10.);
#7194=VECTOR('',#23192,10.);
#7195=VECTOR('',#23195,10.);
#7196=VECTOR('',#23198,10.);
#7197=VECTOR('',#23201,10.);
#7198=VECTOR('',#23204,10.);
#7199=VECTOR('',#23207,10.);
#7200=VECTOR('',#23210,10.);
#7201=VECTOR('',#23213,10.);
#7202=VECTOR('',#23216,10.);
#7203=VECTOR('',#23219,10.);
#7204=VECTOR('',#23222,10.);
#7205=VECTOR('',#23225,10.);
#7206=VECTOR('',#23228,10.);
#7207=VECTOR('',#23231,10.);
#7208=VECTOR('',#23234,10.);
#7209=VECTOR('',#23237,10.);
#7210=VECTOR('',#23240,10.);
#7211=VECTOR('',#23243,10.);
#7212=VECTOR('',#23246,10.);
#7213=VECTOR('',#23249,10.);
#7214=VECTOR('',#23252,10.);
#7215=VECTOR('',#23255,10.);
#7216=VECTOR('',#23258,10.);
#7217=VECTOR('',#23261,10.);
#7218=VECTOR('',#23264,10.);
#7219=VECTOR('',#23267,10.);
#7220=VECTOR('',#23270,10.);
#7221=VECTOR('',#23273,10.);
#7222=VECTOR('',#23276,10.);
#7223=VECTOR('',#23279,10.);
#7224=VECTOR('',#23282,10.);
#7225=VECTOR('',#23285,10.);
#7226=VECTOR('',#23288,10.);
#7227=VECTOR('',#23291,10.);
#7228=VECTOR('',#23294,10.);
#7229=VECTOR('',#23297,10.);
#7230=VECTOR('',#23300,10.);
#7231=VECTOR('',#23303,10.);
#7232=VECTOR('',#23306,10.);
#7233=VECTOR('',#23309,10.);
#7234=VECTOR('',#23312,10.);
#7235=VECTOR('',#23315,10.);
#7236=VECTOR('',#23318,10.);
#7237=VECTOR('',#23321,10.);
#7238=VECTOR('',#23324,10.);
#7239=VECTOR('',#23327,10.);
#7240=VECTOR('',#23330,10.);
#7241=VECTOR('',#23333,10.);
#7242=VECTOR('',#23336,10.);
#7243=VECTOR('',#23339,10.);
#7244=VECTOR('',#23342,10.);
#7245=VECTOR('',#23345,10.);
#7246=VECTOR('',#23348,10.);
#7247=VECTOR('',#23351,10.);
#7248=VECTOR('',#23354,10.);
#7249=VECTOR('',#23357,10.);
#7250=VECTOR('',#23360,10.);
#7251=VECTOR('',#23363,10.);
#7252=VECTOR('',#23366,10.);
#7253=VECTOR('',#23369,10.);
#7254=VECTOR('',#23372,10.);
#7255=VECTOR('',#23375,10.);
#7256=VECTOR('',#23378,10.);
#7257=VECTOR('',#23381,10.);
#7258=VECTOR('',#23384,10.);
#7259=VECTOR('',#23387,10.);
#7260=VECTOR('',#23390,10.);
#7261=VECTOR('',#23393,10.);
#7262=VECTOR('',#23396,10.);
#7263=VECTOR('',#23399,10.);
#7264=VECTOR('',#23402,10.);
#7265=VECTOR('',#23405,10.);
#7266=VECTOR('',#23408,10.);
#7267=VECTOR('',#23411,10.);
#7268=VECTOR('',#23414,10.);
#7269=VECTOR('',#23417,10.);
#7270=VECTOR('',#23420,10.);
#7271=VECTOR('',#23423,10.);
#7272=VECTOR('',#23426,10.);
#7273=VECTOR('',#23429,10.);
#7274=VECTOR('',#23432,10.);
#7275=VECTOR('',#23435,10.);
#7276=VECTOR('',#23438,10.);
#7277=VECTOR('',#23441,10.);
#7278=VECTOR('',#23444,10.);
#7279=VECTOR('',#23447,10.);
#7280=VECTOR('',#23450,10.);
#7281=VECTOR('',#23453,10.);
#7282=VECTOR('',#23456,10.);
#7283=VECTOR('',#23459,10.);
#7284=VECTOR('',#23462,10.);
#7285=VECTOR('',#23465,10.);
#7286=VECTOR('',#23468,10.);
#7287=VECTOR('',#23471,10.);
#7288=VECTOR('',#23474,10.);
#7289=VECTOR('',#23477,10.);
#7290=VECTOR('',#23480,10.);
#7291=VECTOR('',#23483,10.);
#7292=VECTOR('',#23486,10.);
#7293=VECTOR('',#23489,10.);
#7294=VECTOR('',#23492,10.);
#7295=VECTOR('',#23495,10.);
#7296=VECTOR('',#23498,10.);
#7297=VECTOR('',#23501,10.);
#7298=VECTOR('',#23504,10.);
#7299=VECTOR('',#23507,10.);
#7300=VECTOR('',#23510,10.);
#7301=VECTOR('',#23513,10.);
#7302=VECTOR('',#23516,10.);
#7303=VECTOR('',#23519,10.);
#7304=VECTOR('',#23522,10.);
#7305=VECTOR('',#23525,10.);
#7306=VECTOR('',#23528,10.);
#7307=VECTOR('',#23531,10.);
#7308=VECTOR('',#23534,10.);
#7309=VECTOR('',#23537,10.);
#7310=VECTOR('',#23540,10.);
#7311=VECTOR('',#23543,10.);
#7312=VECTOR('',#23546,10.);
#7313=VECTOR('',#23549,10.);
#7314=VECTOR('',#23552,10.);
#7315=VECTOR('',#23555,10.);
#7316=VECTOR('',#23558,10.);
#7317=VECTOR('',#23561,10.);
#7318=VECTOR('',#23564,10.);
#7319=VECTOR('',#23567,10.);
#7320=VECTOR('',#23570,10.);
#7321=VECTOR('',#23573,10.);
#7322=VECTOR('',#23576,10.);
#7323=VECTOR('',#23579,10.);
#8807=VERTEX_POINT('',#59399);
#8808=VERTEX_POINT('',#59401);
#8809=VERTEX_POINT('',#59405);
#8810=VERTEX_POINT('',#59409);
#8811=VERTEX_POINT('',#59410);
#8812=VERTEX_POINT('',#59412);
#8813=VERTEX_POINT('',#59414);
#8814=VERTEX_POINT('',#59416);
#8815=VERTEX_POINT('',#59418);
#8816=VERTEX_POINT('',#59420);
#8817=VERTEX_POINT('',#59422);
#8818=VERTEX_POINT('',#59424);
#8819=VERTEX_POINT('',#59426);
#8820=VERTEX_POINT('',#59428);
#8821=VERTEX_POINT('',#59430);
#8822=VERTEX_POINT('',#59432);
#8823=VERTEX_POINT('',#59434);
#8824=VERTEX_POINT('',#59436);
#8825=VERTEX_POINT('',#59438);
#8826=VERTEX_POINT('',#59440);
#8827=VERTEX_POINT('',#59442);
#8828=VERTEX_POINT('',#59444);
#8829=VERTEX_POINT('',#59446);
#8830=VERTEX_POINT('',#59448);
#8831=VERTEX_POINT('',#59450);
#8832=VERTEX_POINT('',#59452);
#8833=VERTEX_POINT('',#59454);
#8834=VERTEX_POINT('',#59456);
#8835=VERTEX_POINT('',#59458);
#8836=VERTEX_POINT('',#59460);
#8837=VERTEX_POINT('',#59462);
#8838=VERTEX_POINT('',#59464);
#8839=VERTEX_POINT('',#59466);
#8840=VERTEX_POINT('',#59468);
#8841=VERTEX_POINT('',#59470);
#8842=VERTEX_POINT('',#59472);
#8843=VERTEX_POINT('',#59474);
#8844=VERTEX_POINT('',#59476);
#8845=VERTEX_POINT('',#59478);
#8846=VERTEX_POINT('',#59480);
#8847=VERTEX_POINT('',#59482);
#8848=VERTEX_POINT('',#59484);
#8849=VERTEX_POINT('',#59486);
#8850=VERTEX_POINT('',#59488);
#8851=VERTEX_POINT('',#59490);
#8852=VERTEX_POINT('',#59492);
#8853=VERTEX_POINT('',#59494);
#8854=VERTEX_POINT('',#59496);
#8855=VERTEX_POINT('',#59498);
#8856=VERTEX_POINT('',#59500);
#8857=VERTEX_POINT('',#59502);
#8858=VERTEX_POINT('',#59504);
#8859=VERTEX_POINT('',#59506);
#8860=VERTEX_POINT('',#59508);
#8861=VERTEX_POINT('',#59510);
#8862=VERTEX_POINT('',#59512);
#8863=VERTEX_POINT('',#59514);
#8864=VERTEX_POINT('',#59516);
#8865=VERTEX_POINT('',#59518);
#8866=VERTEX_POINT('',#59520);
#8867=VERTEX_POINT('',#59522);
#8868=VERTEX_POINT('',#59524);
#8869=VERTEX_POINT('',#59526);
#8870=VERTEX_POINT('',#59528);
#8871=VERTEX_POINT('',#59530);
#8872=VERTEX_POINT('',#59532);
#8873=VERTEX_POINT('',#59534);
#8874=VERTEX_POINT('',#59536);
#8875=VERTEX_POINT('',#59538);
#8876=VERTEX_POINT('',#59540);
#8877=VERTEX_POINT('',#59542);
#8878=VERTEX_POINT('',#59544);
#8879=VERTEX_POINT('',#59546);
#8880=VERTEX_POINT('',#59548);
#8881=VERTEX_POINT('',#59550);
#8882=VERTEX_POINT('',#59552);
#8883=VERTEX_POINT('',#59554);
#8884=VERTEX_POINT('',#59556);
#8885=VERTEX_POINT('',#59558);
#8886=VERTEX_POINT('',#59560);
#8887=VERTEX_POINT('',#59562);
#8888=VERTEX_POINT('',#59564);
#8889=VERTEX_POINT('',#59566);
#8890=VERTEX_POINT('',#59568);
#8891=VERTEX_POINT('',#59570);
#8892=VERTEX_POINT('',#59572);
#8893=VERTEX_POINT('',#59574);
#8894=VERTEX_POINT('',#59576);
#8895=VERTEX_POINT('',#59578);
#8896=VERTEX_POINT('',#59580);
#8897=VERTEX_POINT('',#59582);
#8898=VERTEX_POINT('',#59584);
#8899=VERTEX_POINT('',#59586);
#8900=VERTEX_POINT('',#59588);
#8901=VERTEX_POINT('',#59590);
#8902=VERTEX_POINT('',#59592);
#8903=VERTEX_POINT('',#59594);
#8904=VERTEX_POINT('',#59596);
#8905=VERTEX_POINT('',#59598);
#8906=VERTEX_POINT('',#59600);
#8907=VERTEX_POINT('',#59602);
#8908=VERTEX_POINT('',#59604);
#8909=VERTEX_POINT('',#59606);
#8910=VERTEX_POINT('',#59608);
#8911=VERTEX_POINT('',#59610);
#8912=VERTEX_POINT('',#59612);
#8913=VERTEX_POINT('',#59614);
#8914=VERTEX_POINT('',#59616);
#8915=VERTEX_POINT('',#59618);
#8916=VERTEX_POINT('',#59620);
#8917=VERTEX_POINT('',#59622);
#8918=VERTEX_POINT('',#59624);
#8919=VERTEX_POINT('',#59626);
#8920=VERTEX_POINT('',#59628);
#8921=VERTEX_POINT('',#59630);
#8922=VERTEX_POINT('',#59632);
#8923=VERTEX_POINT('',#59634);
#8924=VERTEX_POINT('',#59636);
#8925=VERTEX_POINT('',#59638);
#8926=VERTEX_POINT('',#59640);
#8927=VERTEX_POINT('',#59642);
#8928=VERTEX_POINT('',#59644);
#8929=VERTEX_POINT('',#59646);
#8930=VERTEX_POINT('',#59648);
#8931=VERTEX_POINT('',#59650);
#8932=VERTEX_POINT('',#59652);
#8933=VERTEX_POINT('',#59654);
#8934=VERTEX_POINT('',#59656);
#8935=VERTEX_POINT('',#59658);
#8936=VERTEX_POINT('',#59660);
#8937=VERTEX_POINT('',#59662);
#8938=VERTEX_POINT('',#59664);
#8939=VERTEX_POINT('',#59666);
#8940=VERTEX_POINT('',#59668);
#8941=VERTEX_POINT('',#59670);
#8942=VERTEX_POINT('',#59672);
#8943=VERTEX_POINT('',#59674);
#8944=VERTEX_POINT('',#59676);
#8945=VERTEX_POINT('',#59678);
#8946=VERTEX_POINT('',#59680);
#8947=VERTEX_POINT('',#59682);
#8948=VERTEX_POINT('',#59684);
#8949=VERTEX_POINT('',#59686);
#8950=VERTEX_POINT('',#59688);
#8951=VERTEX_POINT('',#59690);
#8952=VERTEX_POINT('',#59692);
#8953=VERTEX_POINT('',#59694);
#8954=VERTEX_POINT('',#59696);
#8955=VERTEX_POINT('',#59698);
#8956=VERTEX_POINT('',#59700);
#8957=VERTEX_POINT('',#59702);
#8958=VERTEX_POINT('',#59704);
#8959=VERTEX_POINT('',#59706);
#8960=VERTEX_POINT('',#59709);
#8961=VERTEX_POINT('',#59712);
#8962=VERTEX_POINT('',#59716);
#8963=VERTEX_POINT('',#59717);
#8964=VERTEX_POINT('',#59719);
#8965=VERTEX_POINT('',#59721);
#8966=VERTEX_POINT('',#59723);
#8967=VERTEX_POINT('',#59725);
#8968=VERTEX_POINT('',#59727);
#8969=VERTEX_POINT('',#59729);
#8970=VERTEX_POINT('',#59731);
#8971=VERTEX_POINT('',#59733);
#8972=VERTEX_POINT('',#59735);
#8973=VERTEX_POINT('',#59737);
#8974=VERTEX_POINT('',#59739);
#8975=VERTEX_POINT('',#59741);
#8976=VERTEX_POINT('',#59743);
#8977=VERTEX_POINT('',#59745);
#8978=VERTEX_POINT('',#59747);
#8979=VERTEX_POINT('',#59749);
#8980=VERTEX_POINT('',#59751);
#8981=VERTEX_POINT('',#59753);
#8982=VERTEX_POINT('',#59755);
#8983=VERTEX_POINT('',#59757);
#8984=VERTEX_POINT('',#59759);
#8985=VERTEX_POINT('',#59761);
#8986=VERTEX_POINT('',#59763);
#8987=VERTEX_POINT('',#59765);
#8988=VERTEX_POINT('',#59767);
#8989=VERTEX_POINT('',#59769);
#8990=VERTEX_POINT('',#59771);
#8991=VERTEX_POINT('',#59773);
#8992=VERTEX_POINT('',#59775);
#8993=VERTEX_POINT('',#59777);
#8994=VERTEX_POINT('',#59779);
#8995=VERTEX_POINT('',#59781);
#8996=VERTEX_POINT('',#59783);
#8997=VERTEX_POINT('',#59785);
#8998=VERTEX_POINT('',#59787);
#8999=VERTEX_POINT('',#59789);
#9000=VERTEX_POINT('',#59791);
#9001=VERTEX_POINT('',#59793);
#9002=VERTEX_POINT('',#59795);
#9003=VERTEX_POINT('',#59797);
#9004=VERTEX_POINT('',#59799);
#9005=VERTEX_POINT('',#59801);
#9006=VERTEX_POINT('',#59803);
#9007=VERTEX_POINT('',#59805);
#9008=VERTEX_POINT('',#59807);
#9009=VERTEX_POINT('',#59809);
#9010=VERTEX_POINT('',#59811);
#9011=VERTEX_POINT('',#59813);
#9012=VERTEX_POINT('',#59815);
#9013=VERTEX_POINT('',#59817);
#9014=VERTEX_POINT('',#59819);
#9015=VERTEX_POINT('',#59821);
#9016=VERTEX_POINT('',#59823);
#9017=VERTEX_POINT('',#59825);
#9018=VERTEX_POINT('',#59827);
#9019=VERTEX_POINT('',#59829);
#9020=VERTEX_POINT('',#59831);
#9021=VERTEX_POINT('',#59833);
#9022=VERTEX_POINT('',#59835);
#9023=VERTEX_POINT('',#59837);
#9024=VERTEX_POINT('',#59839);
#9025=VERTEX_POINT('',#59841);
#9026=VERTEX_POINT('',#59843);
#9027=VERTEX_POINT('',#59845);
#9028=VERTEX_POINT('',#59847);
#9029=VERTEX_POINT('',#59849);
#9030=VERTEX_POINT('',#59851);
#9031=VERTEX_POINT('',#59853);
#9032=VERTEX_POINT('',#59855);
#9033=VERTEX_POINT('',#59857);
#9034=VERTEX_POINT('',#59859);
#9035=VERTEX_POINT('',#59861);
#9036=VERTEX_POINT('',#59863);
#9037=VERTEX_POINT('',#59865);
#9038=VERTEX_POINT('',#59867);
#9039=VERTEX_POINT('',#59869);
#9040=VERTEX_POINT('',#59871);
#9041=VERTEX_POINT('',#59873);
#9042=VERTEX_POINT('',#59875);
#9043=VERTEX_POINT('',#59877);
#9044=VERTEX_POINT('',#59879);
#9045=VERTEX_POINT('',#59881);
#9046=VERTEX_POINT('',#59883);
#9047=VERTEX_POINT('',#59885);
#9048=VERTEX_POINT('',#59887);
#9049=VERTEX_POINT('',#59889);
#9050=VERTEX_POINT('',#59891);
#9051=VERTEX_POINT('',#59893);
#9052=VERTEX_POINT('',#59895);
#9053=VERTEX_POINT('',#59897);
#9054=VERTEX_POINT('',#59899);
#9055=VERTEX_POINT('',#59901);
#9056=VERTEX_POINT('',#59903);
#9057=VERTEX_POINT('',#59905);
#9058=VERTEX_POINT('',#59907);
#9059=VERTEX_POINT('',#59909);
#9060=VERTEX_POINT('',#59911);
#9061=VERTEX_POINT('',#59913);
#9062=VERTEX_POINT('',#59915);
#9063=VERTEX_POINT('',#59917);
#9064=VERTEX_POINT('',#59919);
#9065=VERTEX_POINT('',#59921);
#9066=VERTEX_POINT('',#59923);
#9067=VERTEX_POINT('',#59925);
#9068=VERTEX_POINT('',#59927);
#9069=VERTEX_POINT('',#59929);
#9070=VERTEX_POINT('',#59931);
#9071=VERTEX_POINT('',#59933);
#9072=VERTEX_POINT('',#59935);
#9073=VERTEX_POINT('',#59937);
#9074=VERTEX_POINT('',#59939);
#9075=VERTEX_POINT('',#59941);
#9076=VERTEX_POINT('',#59943);
#9077=VERTEX_POINT('',#59945);
#9078=VERTEX_POINT('',#59947);
#9079=VERTEX_POINT('',#59949);
#9080=VERTEX_POINT('',#59951);
#9081=VERTEX_POINT('',#59953);
#9082=VERTEX_POINT('',#59955);
#9083=VERTEX_POINT('',#59957);
#9084=VERTEX_POINT('',#59959);
#9085=VERTEX_POINT('',#59961);
#9086=VERTEX_POINT('',#59963);
#9087=VERTEX_POINT('',#59965);
#9088=VERTEX_POINT('',#59967);
#9089=VERTEX_POINT('',#59969);
#9090=VERTEX_POINT('',#59971);
#9091=VERTEX_POINT('',#59973);
#9092=VERTEX_POINT('',#59975);
#9093=VERTEX_POINT('',#59977);
#9094=VERTEX_POINT('',#59979);
#9095=VERTEX_POINT('',#59981);
#9096=VERTEX_POINT('',#59983);
#9097=VERTEX_POINT('',#59985);
#9098=VERTEX_POINT('',#59987);
#9099=VERTEX_POINT('',#59989);
#9100=VERTEX_POINT('',#59991);
#9101=VERTEX_POINT('',#59993);
#9102=VERTEX_POINT('',#59995);
#9103=VERTEX_POINT('',#59997);
#9104=VERTEX_POINT('',#59999);
#9105=VERTEX_POINT('',#60001);
#9106=VERTEX_POINT('',#60003);
#9107=VERTEX_POINT('',#60005);
#9108=VERTEX_POINT('',#60007);
#9109=VERTEX_POINT('',#60009);
#9110=VERTEX_POINT('',#60011);
#9111=VERTEX_POINT('',#60013);
#9112=VERTEX_POINT('',#60016);
#9113=VERTEX_POINT('',#60019);
#9114=VERTEX_POINT('',#60023);
#11351=EDGE_CURVE('',#8807,#8807,#3697,.T.);
#11352=EDGE_CURVE('',#8807,#8808,#5456,.T.);
#11353=EDGE_CURVE('',#8808,#8808,#3698,.T.);
#11354=EDGE_CURVE('',#8808,#8809,#5457,.T.);
#11355=EDGE_CURVE('',#8809,#8809,#3699,.T.);
#11356=EDGE_CURVE('',#8810,#8811,#5458,.T.);
#11357=EDGE_CURVE('',#8812,#8810,#5459,.T.);
#11358=EDGE_CURVE('',#8813,#8812,#5460,.T.);
#11359=EDGE_CURVE('',#8814,#8813,#5461,.T.);
#11360=EDGE_CURVE('',#8815,#8814,#5462,.T.);
#11361=EDGE_CURVE('',#8816,#8815,#5463,.T.);
#11362=EDGE_CURVE('',#8817,#8816,#5464,.T.);
#11363=EDGE_CURVE('',#8818,#8817,#5465,.T.);
#11364=EDGE_CURVE('',#8819,#8818,#5466,.T.);
#11365=EDGE_CURVE('',#8820,#8819,#5467,.T.);
#11366=EDGE_CURVE('',#8821,#8820,#5468,.T.);
#11367=EDGE_CURVE('',#8822,#8821,#5469,.T.);
#11368=EDGE_CURVE('',#8823,#8822,#5470,.T.);
#11369=EDGE_CURVE('',#8824,#8823,#5471,.T.);
#11370=EDGE_CURVE('',#8825,#8824,#5472,.T.);
#11371=EDGE_CURVE('',#8826,#8825,#5473,.T.);
#11372=EDGE_CURVE('',#8827,#8826,#5474,.T.);
#11373=EDGE_CURVE('',#8828,#8827,#5475,.T.);
#11374=EDGE_CURVE('',#8829,#8828,#5476,.T.);
#11375=EDGE_CURVE('',#8830,#8829,#5477,.T.);
#11376=EDGE_CURVE('',#8831,#8830,#5478,.T.);
#11377=EDGE_CURVE('',#8832,#8831,#5479,.T.);
#11378=EDGE_CURVE('',#8833,#8832,#5480,.T.);
#11379=EDGE_CURVE('',#8834,#8833,#5481,.T.);
#11380=EDGE_CURVE('',#8835,#8834,#5482,.T.);
#11381=EDGE_CURVE('',#8836,#8835,#5483,.T.);
#11382=EDGE_CURVE('',#8837,#8836,#5484,.T.);
#11383=EDGE_CURVE('',#8838,#8837,#5485,.T.);
#11384=EDGE_CURVE('',#8839,#8838,#5486,.T.);
#11385=EDGE_CURVE('',#8840,#8839,#5487,.T.);
#11386=EDGE_CURVE('',#8841,#8840,#5488,.T.);
#11387=EDGE_CURVE('',#8842,#8841,#5489,.T.);
#11388=EDGE_CURVE('',#8843,#8842,#5490,.T.);
#11389=EDGE_CURVE('',#8844,#8843,#5491,.T.);
#11390=EDGE_CURVE('',#8845,#8844,#5492,.T.);
#11391=EDGE_CURVE('',#8846,#8845,#5493,.T.);
#11392=EDGE_CURVE('',#8847,#8846,#5494,.T.);
#11393=EDGE_CURVE('',#8848,#8847,#5495,.T.);
#11394=EDGE_CURVE('',#8849,#8848,#5496,.T.);
#11395=EDGE_CURVE('',#8850,#8849,#5497,.T.);
#11396=EDGE_CURVE('',#8851,#8850,#5498,.T.);
#11397=EDGE_CURVE('',#8852,#8851,#5499,.T.);
#11398=EDGE_CURVE('',#8853,#8852,#5500,.T.);
#11399=EDGE_CURVE('',#8854,#8853,#5501,.T.);
#11400=EDGE_CURVE('',#8855,#8854,#5502,.T.);
#11401=EDGE_CURVE('',#8856,#8855,#5503,.T.);
#11402=EDGE_CURVE('',#8857,#8856,#5504,.T.);
#11403=EDGE_CURVE('',#8858,#8857,#5505,.T.);
#11404=EDGE_CURVE('',#8859,#8858,#5506,.T.);
#11405=EDGE_CURVE('',#8860,#8859,#5507,.T.);
#11406=EDGE_CURVE('',#8861,#8860,#5508,.T.);
#11407=EDGE_CURVE('',#8862,#8861,#5509,.T.);
#11408=EDGE_CURVE('',#8863,#8862,#5510,.T.);
#11409=EDGE_CURVE('',#8864,#8863,#5511,.T.);
#11410=EDGE_CURVE('',#8865,#8864,#5512,.T.);
#11411=EDGE_CURVE('',#8866,#8865,#5513,.T.);
#11412=EDGE_CURVE('',#8867,#8866,#5514,.T.);
#11413=EDGE_CURVE('',#8868,#8867,#5515,.T.);
#11414=EDGE_CURVE('',#8869,#8868,#5516,.T.);
#11415=EDGE_CURVE('',#8870,#8869,#5517,.T.);
#11416=EDGE_CURVE('',#8871,#8870,#5518,.T.);
#11417=EDGE_CURVE('',#8872,#8871,#5519,.T.);
#11418=EDGE_CURVE('',#8873,#8872,#5520,.T.);
#11419=EDGE_CURVE('',#8874,#8873,#5521,.T.);
#11420=EDGE_CURVE('',#8875,#8874,#5522,.T.);
#11421=EDGE_CURVE('',#8876,#8875,#5523,.T.);
#11422=EDGE_CURVE('',#8877,#8876,#5524,.T.);
#11423=EDGE_CURVE('',#8878,#8877,#5525,.T.);
#11424=EDGE_CURVE('',#8879,#8878,#5526,.T.);
#11425=EDGE_CURVE('',#8880,#8879,#5527,.T.);
#11426=EDGE_CURVE('',#8881,#8880,#5528,.T.);
#11427=EDGE_CURVE('',#8882,#8881,#5529,.T.);
#11428=EDGE_CURVE('',#8883,#8882,#5530,.T.);
#11429=EDGE_CURVE('',#8884,#8883,#5531,.T.);
#11430=EDGE_CURVE('',#8885,#8884,#5532,.T.);
#11431=EDGE_CURVE('',#8886,#8885,#5533,.T.);
#11432=EDGE_CURVE('',#8887,#8886,#5534,.T.);
#11433=EDGE_CURVE('',#8888,#8887,#5535,.T.);
#11434=EDGE_CURVE('',#8889,#8888,#5536,.T.);
#11435=EDGE_CURVE('',#8890,#8889,#5537,.T.);
#11436=EDGE_CURVE('',#8891,#8890,#5538,.T.);
#11437=EDGE_CURVE('',#8892,#8891,#5539,.T.);
#11438=EDGE_CURVE('',#8893,#8892,#5540,.T.);
#11439=EDGE_CURVE('',#8894,#8893,#5541,.T.);
#11440=EDGE_CURVE('',#8895,#8894,#5542,.T.);
#11441=EDGE_CURVE('',#8896,#8895,#5543,.T.);
#11442=EDGE_CURVE('',#8897,#8896,#5544,.T.);
#11443=EDGE_CURVE('',#8898,#8897,#5545,.T.);
#11444=EDGE_CURVE('',#8899,#8898,#5546,.T.);
#11445=EDGE_CURVE('',#8900,#8899,#5547,.T.);
#11446=EDGE_CURVE('',#8901,#8900,#5548,.T.);
#11447=EDGE_CURVE('',#8902,#8901,#5549,.T.);
#11448=EDGE_CURVE('',#8903,#8902,#5550,.T.);
#11449=EDGE_CURVE('',#8904,#8903,#5551,.T.);
#11450=EDGE_CURVE('',#8905,#8904,#5552,.T.);
#11451=EDGE_CURVE('',#8906,#8905,#5553,.T.);
#11452=EDGE_CURVE('',#8907,#8906,#5554,.T.);
#11453=EDGE_CURVE('',#8908,#8907,#5555,.T.);
#11454=EDGE_CURVE('',#8909,#8908,#5556,.T.);
#11455=EDGE_CURVE('',#8910,#8909,#5557,.T.);
#11456=EDGE_CURVE('',#8911,#8910,#5558,.T.);
#11457=EDGE_CURVE('',#8912,#8911,#5559,.T.);
#11458=EDGE_CURVE('',#8913,#8912,#5560,.T.);
#11459=EDGE_CURVE('',#8914,#8913,#5561,.T.);
#11460=EDGE_CURVE('',#8915,#8914,#5562,.T.);
#11461=EDGE_CURVE('',#8916,#8915,#5563,.T.);
#11462=EDGE_CURVE('',#8917,#8916,#5564,.T.);
#11463=EDGE_CURVE('',#8918,#8917,#5565,.T.);
#11464=EDGE_CURVE('',#8919,#8918,#5566,.T.);
#11465=EDGE_CURVE('',#8920,#8919,#5567,.T.);
#11466=EDGE_CURVE('',#8921,#8920,#5568,.T.);
#11467=EDGE_CURVE('',#8922,#8921,#5569,.T.);
#11468=EDGE_CURVE('',#8923,#8922,#5570,.T.);
#11469=EDGE_CURVE('',#8924,#8923,#5571,.T.);
#11470=EDGE_CURVE('',#8925,#8924,#5572,.T.);
#11471=EDGE_CURVE('',#8926,#8925,#5573,.T.);
#11472=EDGE_CURVE('',#8927,#8926,#5574,.T.);
#11473=EDGE_CURVE('',#8928,#8927,#5575,.T.);
#11474=EDGE_CURVE('',#8929,#8928,#5576,.T.);
#11475=EDGE_CURVE('',#8930,#8929,#5577,.T.);
#11476=EDGE_CURVE('',#8931,#8930,#5578,.T.);
#11477=EDGE_CURVE('',#8932,#8931,#5579,.T.);
#11478=EDGE_CURVE('',#8933,#8932,#5580,.T.);
#11479=EDGE_CURVE('',#8934,#8933,#5581,.T.);
#11480=EDGE_CURVE('',#8935,#8934,#5582,.T.);
#11481=EDGE_CURVE('',#8936,#8935,#5583,.T.);
#11482=EDGE_CURVE('',#8937,#8936,#5584,.T.);
#11483=EDGE_CURVE('',#8938,#8937,#5585,.T.);
#11484=EDGE_CURVE('',#8939,#8938,#5586,.T.);
#11485=EDGE_CURVE('',#8940,#8939,#5587,.T.);
#11486=EDGE_CURVE('',#8941,#8940,#5588,.T.);
#11487=EDGE_CURVE('',#8942,#8941,#5589,.T.);
#11488=EDGE_CURVE('',#8943,#8942,#5590,.T.);
#11489=EDGE_CURVE('',#8944,#8943,#5591,.T.);
#11490=EDGE_CURVE('',#8945,#8944,#5592,.T.);
#11491=EDGE_CURVE('',#8946,#8945,#5593,.T.);
#11492=EDGE_CURVE('',#8947,#8946,#5594,.T.);
#11493=EDGE_CURVE('',#8948,#8947,#5595,.T.);
#11494=EDGE_CURVE('',#8949,#8948,#5596,.T.);
#11495=EDGE_CURVE('',#8950,#8949,#5597,.T.);
#11496=EDGE_CURVE('',#8951,#8950,#5598,.T.);
#11497=EDGE_CURVE('',#8952,#8951,#5599,.T.);
#11498=EDGE_CURVE('',#8953,#8952,#5600,.T.);
#11499=EDGE_CURVE('',#8954,#8953,#5601,.T.);
#11500=EDGE_CURVE('',#8955,#8954,#5602,.T.);
#11501=EDGE_CURVE('',#8956,#8955,#5603,.T.);
#11502=EDGE_CURVE('',#8957,#8956,#5604,.T.);
#11503=EDGE_CURVE('',#8958,#8957,#5605,.T.);
#11504=EDGE_CURVE('',#8959,#8958,#5606,.T.);
#11505=EDGE_CURVE('',#8811,#8959,#5607,.T.);
#11506=EDGE_CURVE('',#8960,#8960,#3700,.T.);
#11507=EDGE_CURVE('',#8961,#8961,#3701,.T.);
#11508=EDGE_CURVE('',#8961,#8809,#5608,.T.);
#11509=EDGE_CURVE('',#8962,#8963,#5609,.T.);
#11510=EDGE_CURVE('',#8963,#8964,#5610,.T.);
#11511=EDGE_CURVE('',#8964,#8965,#5611,.T.);
#11512=EDGE_CURVE('',#8965,#8966,#5612,.T.);
#11513=EDGE_CURVE('',#8966,#8967,#5613,.T.);
#11514=EDGE_CURVE('',#8967,#8968,#5614,.T.);
#11515=EDGE_CURVE('',#8968,#8969,#5615,.T.);
#11516=EDGE_CURVE('',#8969,#8970,#5616,.T.);
#11517=EDGE_CURVE('',#8970,#8971,#5617,.T.);
#11518=EDGE_CURVE('',#8971,#8972,#5618,.T.);
#11519=EDGE_CURVE('',#8972,#8973,#5619,.T.);
#11520=EDGE_CURVE('',#8973,#8974,#5620,.T.);
#11521=EDGE_CURVE('',#8974,#8975,#5621,.T.);
#11522=EDGE_CURVE('',#8975,#8976,#5622,.T.);
#11523=EDGE_CURVE('',#8976,#8977,#5623,.T.);
#11524=EDGE_CURVE('',#8977,#8978,#5624,.T.);
#11525=EDGE_CURVE('',#8978,#8979,#5625,.T.);
#11526=EDGE_CURVE('',#8979,#8980,#5626,.T.);
#11527=EDGE_CURVE('',#8980,#8981,#5627,.T.);
#11528=EDGE_CURVE('',#8981,#8982,#5628,.T.);
#11529=EDGE_CURVE('',#8982,#8983,#5629,.T.);
#11530=EDGE_CURVE('',#8983,#8984,#5630,.T.);
#11531=EDGE_CURVE('',#8984,#8985,#5631,.T.);
#11532=EDGE_CURVE('',#8985,#8986,#5632,.T.);
#11533=EDGE_CURVE('',#8986,#8987,#5633,.T.);
#11534=EDGE_CURVE('',#8987,#8988,#5634,.T.);
#11535=EDGE_CURVE('',#8988,#8989,#5635,.T.);
#11536=EDGE_CURVE('',#8989,#8990,#5636,.T.);
#11537=EDGE_CURVE('',#8990,#8991,#5637,.T.);
#11538=EDGE_CURVE('',#8991,#8992,#5638,.T.);
#11539=EDGE_CURVE('',#8992,#8993,#5639,.T.);
#11540=EDGE_CURVE('',#8993,#8994,#5640,.T.);
#11541=EDGE_CURVE('',#8994,#8995,#5641,.T.);
#11542=EDGE_CURVE('',#8995,#8996,#5642,.T.);
#11543=EDGE_CURVE('',#8996,#8997,#5643,.T.);
#11544=EDGE_CURVE('',#8997,#8998,#5644,.T.);
#11545=EDGE_CURVE('',#8998,#8999,#5645,.T.);
#11546=EDGE_CURVE('',#8999,#9000,#5646,.T.);
#11547=EDGE_CURVE('',#9000,#9001,#5647,.T.);
#11548=EDGE_CURVE('',#9001,#9002,#5648,.T.);
#11549=EDGE_CURVE('',#9002,#9003,#5649,.T.);
#11550=EDGE_CURVE('',#9003,#9004,#5650,.T.);
#11551=EDGE_CURVE('',#9004,#9005,#5651,.T.);
#11552=EDGE_CURVE('',#9005,#9006,#5652,.T.);
#11553=EDGE_CURVE('',#9006,#9007,#5653,.T.);
#11554=EDGE_CURVE('',#9007,#9008,#5654,.T.);
#11555=EDGE_CURVE('',#9008,#9009,#5655,.T.);
#11556=EDGE_CURVE('',#9009,#9010,#5656,.T.);
#11557=EDGE_CURVE('',#9010,#9011,#5657,.T.);
#11558=EDGE_CURVE('',#9011,#9012,#5658,.T.);
#11559=EDGE_CURVE('',#9012,#9013,#5659,.T.);
#11560=EDGE_CURVE('',#9013,#9014,#5660,.T.);
#11561=EDGE_CURVE('',#9014,#9015,#5661,.T.);
#11562=EDGE_CURVE('',#9015,#9016,#5662,.T.);
#11563=EDGE_CURVE('',#9016,#9017,#5663,.T.);
#11564=EDGE_CURVE('',#9017,#9018,#5664,.T.);
#11565=EDGE_CURVE('',#9018,#9019,#5665,.T.);
#11566=EDGE_CURVE('',#9019,#9020,#5666,.T.);
#11567=EDGE_CURVE('',#9020,#9021,#5667,.T.);
#11568=EDGE_CURVE('',#9021,#9022,#5668,.T.);
#11569=EDGE_CURVE('',#9022,#9023,#5669,.T.);
#11570=EDGE_CURVE('',#9023,#9024,#5670,.T.);
#11571=EDGE_CURVE('',#9024,#9025,#5671,.T.);
#11572=EDGE_CURVE('',#9025,#9026,#5672,.T.);
#11573=EDGE_CURVE('',#9026,#9027,#5673,.T.);
#11574=EDGE_CURVE('',#9027,#9028,#5674,.T.);
#11575=EDGE_CURVE('',#9028,#9029,#5675,.T.);
#11576=EDGE_CURVE('',#9029,#9030,#5676,.T.);
#11577=EDGE_CURVE('',#9030,#9031,#5677,.T.);
#11578=EDGE_CURVE('',#9031,#9032,#5678,.T.);
#11579=EDGE_CURVE('',#9032,#9033,#5679,.T.);
#11580=EDGE_CURVE('',#9033,#9034,#5680,.T.);
#11581=EDGE_CURVE('',#9034,#9035,#5681,.T.);
#11582=EDGE_CURVE('',#9035,#9036,#5682,.T.);
#11583=EDGE_CURVE('',#9036,#9037,#5683,.T.);
#11584=EDGE_CURVE('',#9037,#9038,#5684,.T.);
#11585=EDGE_CURVE('',#9038,#9039,#5685,.T.);
#11586=EDGE_CURVE('',#9039,#9040,#5686,.T.);
#11587=EDGE_CURVE('',#9040,#9041,#5687,.T.);
#11588=EDGE_CURVE('',#9041,#9042,#5688,.T.);
#11589=EDGE_CURVE('',#9042,#9043,#5689,.T.);
#11590=EDGE_CURVE('',#9043,#9044,#5690,.T.);
#11591=EDGE_CURVE('',#9044,#9045,#5691,.T.);
#11592=EDGE_CURVE('',#9045,#9046,#5692,.T.);
#11593=EDGE_CURVE('',#9046,#9047,#5693,.T.);
#11594=EDGE_CURVE('',#9047,#9048,#5694,.T.);
#11595=EDGE_CURVE('',#9048,#9049,#5695,.T.);
#11596=EDGE_CURVE('',#9049,#9050,#5696,.T.);
#11597=EDGE_CURVE('',#9050,#9051,#5697,.T.);
#11598=EDGE_CURVE('',#9051,#9052,#5698,.T.);
#11599=EDGE_CURVE('',#9052,#9053,#5699,.T.);
#11600=EDGE_CURVE('',#9053,#9054,#5700,.T.);
#11601=EDGE_CURVE('',#9054,#9055,#5701,.T.);
#11602=EDGE_CURVE('',#9055,#9056,#5702,.T.);
#11603=EDGE_CURVE('',#9056,#9057,#5703,.T.);
#11604=EDGE_CURVE('',#9057,#9058,#5704,.T.);
#11605=EDGE_CURVE('',#9058,#9059,#5705,.T.);
#11606=EDGE_CURVE('',#9059,#9060,#5706,.T.);
#11607=EDGE_CURVE('',#9060,#9061,#5707,.T.);
#11608=EDGE_CURVE('',#9061,#9062,#5708,.T.);
#11609=EDGE_CURVE('',#9062,#9063,#5709,.T.);
#11610=EDGE_CURVE('',#9063,#9064,#5710,.T.);
#11611=EDGE_CURVE('',#9064,#9065,#5711,.T.);
#11612=EDGE_CURVE('',#9065,#9066,#5712,.T.);
#11613=EDGE_CURVE('',#9066,#9067,#5713,.T.);
#11614=EDGE_CURVE('',#9067,#9068,#5714,.T.);
#11615=EDGE_CURVE('',#9068,#9069,#5715,.T.);
#11616=EDGE_CURVE('',#9069,#9070,#5716,.T.);
#11617=EDGE_CURVE('',#9070,#9071,#5717,.T.);
#11618=EDGE_CURVE('',#9071,#9072,#5718,.T.);
#11619=EDGE_CURVE('',#9072,#9073,#5719,.T.);
#11620=EDGE_CURVE('',#9073,#9074,#5720,.T.);
#11621=EDGE_CURVE('',#9074,#9075,#5721,.T.);
#11622=EDGE_CURVE('',#9075,#9076,#5722,.T.);
#11623=EDGE_CURVE('',#9076,#9077,#5723,.T.);
#11624=EDGE_CURVE('',#9077,#9078,#5724,.T.);
#11625=EDGE_CURVE('',#9078,#9079,#5725,.T.);
#11626=EDGE_CURVE('',#9079,#9080,#5726,.T.);
#11627=EDGE_CURVE('',#9080,#9081,#5727,.T.);
#11628=EDGE_CURVE('',#9081,#9082,#5728,.T.);
#11629=EDGE_CURVE('',#9082,#9083,#5729,.T.);
#11630=EDGE_CURVE('',#9083,#9084,#5730,.T.);
#11631=EDGE_CURVE('',#9084,#9085,#5731,.T.);
#11632=EDGE_CURVE('',#9085,#9086,#5732,.T.);
#11633=EDGE_CURVE('',#9086,#9087,#5733,.T.);
#11634=EDGE_CURVE('',#9087,#9088,#5734,.T.);
#11635=EDGE_CURVE('',#9088,#9089,#5735,.T.);
#11636=EDGE_CURVE('',#9089,#9090,#5736,.T.);
#11637=EDGE_CURVE('',#9090,#9091,#5737,.T.);
#11638=EDGE_CURVE('',#9091,#9092,#5738,.T.);
#11639=EDGE_CURVE('',#9092,#9093,#5739,.T.);
#11640=EDGE_CURVE('',#9093,#9094,#5740,.T.);
#11641=EDGE_CURVE('',#9094,#9095,#5741,.T.);
#11642=EDGE_CURVE('',#9095,#9096,#5742,.T.);
#11643=EDGE_CURVE('',#9096,#9097,#5743,.T.);
#11644=EDGE_CURVE('',#9097,#9098,#5744,.T.);
#11645=EDGE_CURVE('',#9098,#9099,#5745,.T.);
#11646=EDGE_CURVE('',#9099,#9100,#5746,.T.);
#11647=EDGE_CURVE('',#9100,#9101,#5747,.T.);
#11648=EDGE_CURVE('',#9101,#9102,#5748,.T.);
#11649=EDGE_CURVE('',#9102,#9103,#5749,.T.);
#11650=EDGE_CURVE('',#9103,#9104,#5750,.T.);
#11651=EDGE_CURVE('',#9104,#9105,#5751,.T.);
#11652=EDGE_CURVE('',#9105,#9106,#5752,.T.);
#11653=EDGE_CURVE('',#9106,#9107,#5753,.T.);
#11654=EDGE_CURVE('',#9107,#9108,#5754,.T.);
#11655=EDGE_CURVE('',#9108,#9109,#5755,.T.);
#11656=EDGE_CURVE('',#9109,#9110,#5756,.T.);
#11657=EDGE_CURVE('',#9110,#9111,#5757,.T.);
#11658=EDGE_CURVE('',#9111,#8962,#5758,.T.);
#11659=EDGE_CURVE('',#9112,#9112,#3702,.T.);
#11660=EDGE_CURVE('',#8960,#9113,#5759,.T.);
#11661=EDGE_CURVE('',#9113,#9113,#3703,.T.);
#11662=EDGE_CURVE('',#9113,#9114,#5760,.T.);
#11663=EDGE_CURVE('',#9114,#9114,#3704,.T.);
#11664=EDGE_CURVE('',#9112,#9114,#5761,.T.);
#11665=EDGE_CURVE('',#8810,#8962,#5762,.T.);
#11666=EDGE_CURVE('',#8812,#9111,#5763,.T.);
#11667=EDGE_CURVE('',#8813,#9110,#5764,.T.);
#11668=EDGE_CURVE('',#8814,#9109,#5765,.T.);
#11669=EDGE_CURVE('',#8815,#9108,#5766,.T.);
#11670=EDGE_CURVE('',#8816,#9107,#5767,.T.);
#11671=EDGE_CURVE('',#8817,#9106,#5768,.T.);
#11672=EDGE_CURVE('',#8818,#9105,#5769,.T.);
#11673=EDGE_CURVE('',#8819,#9104,#5770,.T.);
#11674=EDGE_CURVE('',#8820,#9103,#5771,.T.);
#11675=EDGE_CURVE('',#8821,#9102,#5772,.T.);
#11676=EDGE_CURVE('',#8822,#9101,#5773,.T.);
#11677=EDGE_CURVE('',#8823,#9100,#5774,.T.);
#11678=EDGE_CURVE('',#8824,#9099,#5775,.T.);
#11679=EDGE_CURVE('',#8825,#9098,#5776,.T.);
#11680=EDGE_CURVE('',#8826,#9097,#5777,.T.);
#11681=EDGE_CURVE('',#8827,#9096,#5778,.T.);
#11682=EDGE_CURVE('',#8828,#9095,#5779,.T.);
#11683=EDGE_CURVE('',#8829,#9094,#5780,.T.);
#11684=EDGE_CURVE('',#8830,#9093,#5781,.T.);
#11685=EDGE_CURVE('',#8831,#9092,#5782,.T.);
#11686=EDGE_CURVE('',#8832,#9091,#5783,.T.);
#11687=EDGE_CURVE('',#8833,#9090,#5784,.T.);
#11688=EDGE_CURVE('',#8834,#9089,#5785,.T.);
#11689=EDGE_CURVE('',#8835,#9088,#5786,.T.);
#11690=EDGE_CURVE('',#8836,#9087,#5787,.T.);
#11691=EDGE_CURVE('',#8837,#9086,#5788,.T.);
#11692=EDGE_CURVE('',#8838,#9085,#5789,.T.);
#11693=EDGE_CURVE('',#8839,#9084,#5790,.T.);
#11694=EDGE_CURVE('',#8840,#9083,#5791,.T.);
#11695=EDGE_CURVE('',#8841,#9082,#5792,.T.);
#11696=EDGE_CURVE('',#8842,#9081,#5793,.T.);
#11697=EDGE_CURVE('',#8843,#9080,#5794,.T.);
#11698=EDGE_CURVE('',#8844,#9079,#5795,.T.);
#11699=EDGE_CURVE('',#8845,#9078,#5796,.T.);
#11700=EDGE_CURVE('',#8846,#9077,#5797,.T.);
#11701=EDGE_CURVE('',#8847,#9076,#5798,.T.);
#11702=EDGE_CURVE('',#8848,#9075,#5799,.T.);
#11703=EDGE_CURVE('',#8849,#9074,#5800,.T.);
#11704=EDGE_CURVE('',#8850,#9073,#5801,.T.);
#11705=EDGE_CURVE('',#8851,#9072,#5802,.T.);
#11706=EDGE_CURVE('',#8852,#9071,#5803,.T.);
#11707=EDGE_CURVE('',#8853,#9070,#5804,.T.);
#11708=EDGE_CURVE('',#8854,#9069,#5805,.T.);
#11709=EDGE_CURVE('',#8855,#9068,#5806,.T.);
#11710=EDGE_CURVE('',#8856,#9067,#5807,.T.);
#11711=EDGE_CURVE('',#8857,#9066,#5808,.T.);
#11712=EDGE_CURVE('',#8858,#9065,#5809,.T.);
#11713=EDGE_CURVE('',#8859,#9064,#5810,.T.);
#11714=EDGE_CURVE('',#8860,#9063,#5811,.T.);
#11715=EDGE_CURVE('',#8861,#9062,#5812,.T.);
#11716=EDGE_CURVE('',#8862,#9061,#5813,.T.);
#11717=EDGE_CURVE('',#8863,#9060,#5814,.T.);
#11718=EDGE_CURVE('',#8864,#9059,#5815,.T.);
#11719=EDGE_CURVE('',#8865,#9058,#5816,.T.);
#11720=EDGE_CURVE('',#8866,#9057,#5817,.T.);
#11721=EDGE_CURVE('',#8867,#9056,#5818,.T.);
#11722=EDGE_CURVE('',#8868,#9055,#5819,.T.);
#11723=EDGE_CURVE('',#8869,#9054,#5820,.T.);
#11724=EDGE_CURVE('',#8870,#9053,#5821,.T.);
#11725=EDGE_CURVE('',#8871,#9052,#5822,.T.);
#11726=EDGE_CURVE('',#8872,#9051,#5823,.T.);
#11727=EDGE_CURVE('',#8873,#9050,#5824,.T.);
#11728=EDGE_CURVE('',#8874,#9049,#5825,.T.);
#11729=EDGE_CURVE('',#8875,#9048,#5826,.T.);
#11730=EDGE_CURVE('',#8876,#9047,#5827,.T.);
#11731=EDGE_CURVE('',#8877,#9046,#5828,.T.);
#11732=EDGE_CURVE('',#8878,#9045,#5829,.T.);
#11733=EDGE_CURVE('',#8879,#9044,#5830,.T.);
#11734=EDGE_CURVE('',#8880,#9043,#5831,.T.);
#11735=EDGE_CURVE('',#8881,#9042,#5832,.T.);
#11736=EDGE_CURVE('',#8882,#9041,#5833,.T.);
#11737=EDGE_CURVE('',#8883,#9040,#5834,.T.);
#11738=EDGE_CURVE('',#8884,#9039,#5835,.T.);
#11739=EDGE_CURVE('',#8885,#9038,#5836,.T.);
#11740=EDGE_CURVE('',#8886,#9037,#5837,.T.);
#11741=EDGE_CURVE('',#8887,#9036,#5838,.T.);
#11742=EDGE_CURVE('',#8888,#9035,#5839,.T.);
#11743=EDGE_CURVE('',#8889,#9034,#5840,.T.);
#11744=EDGE_CURVE('',#8890,#9033,#5841,.T.);
#11745=EDGE_CURVE('',#8891,#9032,#5842,.T.);
#11746=EDGE_CURVE('',#8892,#9031,#5843,.T.);
#11747=EDGE_CURVE('',#8893,#9030,#5844,.T.);
#11748=EDGE_CURVE('',#8894,#9029,#5845,.T.);
#11749=EDGE_CURVE('',#8895,#9028,#5846,.T.);
#11750=EDGE_CURVE('',#8896,#9027,#5847,.T.);
#11751=EDGE_CURVE('',#8897,#9026,#5848,.T.);
#11752=EDGE_CURVE('',#8898,#9025,#5849,.T.);
#11753=EDGE_CURVE('',#8899,#9024,#5850,.T.);
#11754=EDGE_CURVE('',#8900,#9023,#5851,.T.);
#11755=EDGE_CURVE('',#8901,#9022,#5852,.T.);
#11756=EDGE_CURVE('',#8902,#9021,#5853,.T.);
#11757=EDGE_CURVE('',#8903,#9020,#5854,.T.);
#11758=EDGE_CURVE('',#8904,#9019,#5855,.T.);
#11759=EDGE_CURVE('',#8905,#9018,#5856,.T.);
#11760=EDGE_CURVE('',#8906,#9017,#5857,.T.);
#11761=EDGE_CURVE('',#8907,#9016,#5858,.T.);
#11762=EDGE_CURVE('',#8908,#9015,#5859,.T.);
#11763=EDGE_CURVE('',#8909,#9014,#5860,.T.);
#11764=EDGE_CURVE('',#8910,#9013,#5861,.T.);
#11765=EDGE_CURVE('',#8911,#9012,#5862,.T.);
#11766=EDGE_CURVE('',#8912,#9011,#5863,.T.);
#11767=EDGE_CURVE('',#8913,#9010,#5864,.T.);
#11768=EDGE_CURVE('',#8914,#9009,#5865,.T.);
#11769=EDGE_CURVE('',#8915,#9008,#5866,.T.);
#11770=EDGE_CURVE('',#8916,#9007,#5867,.T.);
#11771=EDGE_CURVE('',#8917,#9006,#5868,.T.);
#11772=EDGE_CURVE('',#8918,#9005,#5869,.T.);
#11773=EDGE_CURVE('',#8919,#9004,#5870,.T.);
#11774=EDGE_CURVE('',#8920,#9003,#5871,.T.);
#11775=EDGE_CURVE('',#8921,#9002,#5872,.T.);
#11776=EDGE_CURVE('',#8922,#9001,#5873,.T.);
#11777=EDGE_CURVE('',#8923,#9000,#5874,.T.);
#11778=EDGE_CURVE('',#8924,#8999,#5875,.T.);
#11779=EDGE_CURVE('',#8925,#8998,#5876,.T.);
#11780=EDGE_CURVE('',#8926,#8997,#5877,.T.);
#11781=EDGE_CURVE('',#8927,#8996,#5878,.T.);
#11782=EDGE_CURVE('',#8928,#8995,#5879,.T.);
#11783=EDGE_CURVE('',#8929,#8994,#5880,.T.);
#11784=EDGE_CURVE('',#8930,#8993,#5881,.T.);
#11785=EDGE_CURVE('',#8931,#8992,#5882,.T.);
#11786=EDGE_CURVE('',#8932,#8991,#5883,.T.);
#11787=EDGE_CURVE('',#8933,#8990,#5884,.T.);
#11788=EDGE_CURVE('',#8934,#8989,#5885,.T.);
#11789=EDGE_CURVE('',#8935,#8988,#5886,.T.);
#11790=EDGE_CURVE('',#8936,#8987,#5887,.T.);
#11791=EDGE_CURVE('',#8937,#8986,#5888,.T.);
#11792=EDGE_CURVE('',#8938,#8985,#5889,.T.);
#11793=EDGE_CURVE('',#8939,#8984,#5890,.T.);
#11794=EDGE_CURVE('',#8940,#8983,#5891,.T.);
#11795=EDGE_CURVE('',#8941,#8982,#5892,.T.);
#11796=EDGE_CURVE('',#8942,#8981,#5893,.T.);
#11797=EDGE_CURVE('',#8943,#8980,#5894,.T.);
#11798=EDGE_CURVE('',#8944,#8979,#5895,.T.);
#11799=EDGE_CURVE('',#8945,#8978,#5896,.T.);
#11800=EDGE_CURVE('',#8946,#8977,#5897,.T.);
#11801=EDGE_CURVE('',#8947,#8976,#5898,.T.);
#11802=EDGE_CURVE('',#8948,#8975,#5899,.T.);
#11803=EDGE_CURVE('',#8949,#8974,#5900,.T.);
#11804=EDGE_CURVE('',#8950,#8973,#5901,.T.);
#11805=EDGE_CURVE('',#8951,#8972,#5902,.T.);
#11806=EDGE_CURVE('',#8952,#8971,#5903,.T.);
#11807=EDGE_CURVE('',#8953,#8970,#5904,.T.);
#11808=EDGE_CURVE('',#8954,#8969,#5905,.T.);
#11809=EDGE_CURVE('',#8955,#8968,#5906,.T.);
#11810=EDGE_CURVE('',#8956,#8967,#5907,.T.);
#11811=EDGE_CURVE('',#8957,#8966,#5908,.T.);
#11812=EDGE_CURVE('',#8958,#8965,#5909,.T.);
#11813=EDGE_CURVE('',#8959,#8964,#5910,.T.);
#11814=EDGE_CURVE('',#8811,#8963,#5911,.T.);
#16287=ORIENTED_EDGE('',*,*,#11351,.T.);
#16288=ORIENTED_EDGE('',*,*,#11352,.T.);
#16289=ORIENTED_EDGE('',*,*,#11353,.T.);
#16290=ORIENTED_EDGE('',*,*,#11352,.F.);
#16291=ORIENTED_EDGE('',*,*,#11353,.F.);
#16292=ORIENTED_EDGE('',*,*,#11354,.T.);
#16293=ORIENTED_EDGE('',*,*,#11355,.F.);
#16294=ORIENTED_EDGE('',*,*,#11354,.F.);
#16295=ORIENTED_EDGE('',*,*,#11356,.F.);
#16296=ORIENTED_EDGE('',*,*,#11357,.F.);
#16297=ORIENTED_EDGE('',*,*,#11358,.F.);
#16298=ORIENTED_EDGE('',*,*,#11359,.F.);
#16299=ORIENTED_EDGE('',*,*,#11360,.F.);
#16300=ORIENTED_EDGE('',*,*,#11361,.F.);
#16301=ORIENTED_EDGE('',*,*,#11362,.F.);
#16302=ORIENTED_EDGE('',*,*,#11363,.F.);
#16303=ORIENTED_EDGE('',*,*,#11364,.F.);
#16304=ORIENTED_EDGE('',*,*,#11365,.F.);
#16305=ORIENTED_EDGE('',*,*,#11366,.F.);
#16306=ORIENTED_EDGE('',*,*,#11367,.F.);
#16307=ORIENTED_EDGE('',*,*,#11368,.F.);
#16308=ORIENTED_EDGE('',*,*,#11369,.F.);
#16309=ORIENTED_EDGE('',*,*,#11370,.F.);
#16310=ORIENTED_EDGE('',*,*,#11371,.F.);
#16311=ORIENTED_EDGE('',*,*,#11372,.F.);
#16312=ORIENTED_EDGE('',*,*,#11373,.F.);
#16313=ORIENTED_EDGE('',*,*,#11374,.F.);
#16314=ORIENTED_EDGE('',*,*,#11375,.F.);
#16315=ORIENTED_EDGE('',*,*,#11376,.F.);
#16316=ORIENTED_EDGE('',*,*,#11377,.F.);
#16317=ORIENTED_EDGE('',*,*,#11378,.F.);
#16318=ORIENTED_EDGE('',*,*,#11379,.F.);
#16319=ORIENTED_EDGE('',*,*,#11380,.F.);
#16320=ORIENTED_EDGE('',*,*,#11381,.F.);
#16321=ORIENTED_EDGE('',*,*,#11382,.F.);
#16322=ORIENTED_EDGE('',*,*,#11383,.F.);
#16323=ORIENTED_EDGE('',*,*,#11384,.F.);
#16324=ORIENTED_EDGE('',*,*,#11385,.F.);
#16325=ORIENTED_EDGE('',*,*,#11386,.F.);
#16326=ORIENTED_EDGE('',*,*,#11387,.F.);
#16327=ORIENTED_EDGE('',*,*,#11388,.F.);
#16328=ORIENTED_EDGE('',*,*,#11389,.F.);
#16329=ORIENTED_EDGE('',*,*,#11390,.F.);
#16330=ORIENTED_EDGE('',*,*,#11391,.F.);
#16331=ORIENTED_EDGE('',*,*,#11392,.F.);
#16332=ORIENTED_EDGE('',*,*,#11393,.F.);
#16333=ORIENTED_EDGE('',*,*,#11394,.F.);
#16334=ORIENTED_EDGE('',*,*,#11395,.F.);
#16335=ORIENTED_EDGE('',*,*,#11396,.F.);
#16336=ORIENTED_EDGE('',*,*,#11397,.F.);
#16337=ORIENTED_EDGE('',*,*,#11398,.F.);
#16338=ORIENTED_EDGE('',*,*,#11399,.F.);
#16339=ORIENTED_EDGE('',*,*,#11400,.F.);
#16340=ORIENTED_EDGE('',*,*,#11401,.F.);
#16341=ORIENTED_EDGE('',*,*,#11402,.F.);
#16342=ORIENTED_EDGE('',*,*,#11403,.F.);
#16343=ORIENTED_EDGE('',*,*,#11404,.F.);
#16344=ORIENTED_EDGE('',*,*,#11405,.F.);
#16345=ORIENTED_EDGE('',*,*,#11406,.F.);
#16346=ORIENTED_EDGE('',*,*,#11407,.F.);
#16347=ORIENTED_EDGE('',*,*,#11408,.F.);
#16348=ORIENTED_EDGE('',*,*,#11409,.F.);
#16349=ORIENTED_EDGE('',*,*,#11410,.F.);
#16350=ORIENTED_EDGE('',*,*,#11411,.F.);
#16351=ORIENTED_EDGE('',*,*,#11412,.F.);
#16352=ORIENTED_EDGE('',*,*,#11413,.F.);
#16353=ORIENTED_EDGE('',*,*,#11414,.F.);
#16354=ORIENTED_EDGE('',*,*,#11415,.F.);
#16355=ORIENTED_EDGE('',*,*,#11416,.F.);
#16356=ORIENTED_EDGE('',*,*,#11417,.F.);
#16357=ORIENTED_EDGE('',*,*,#11418,.F.);
#16358=ORIENTED_EDGE('',*,*,#11419,.F.);
#16359=ORIENTED_EDGE('',*,*,#11420,.F.);
#16360=ORIENTED_EDGE('',*,*,#11421,.F.);
#16361=ORIENTED_EDGE('',*,*,#11422,.F.);
#16362=ORIENTED_EDGE('',*,*,#11423,.F.);
#16363=ORIENTED_EDGE('',*,*,#11424,.F.);
#16364=ORIENTED_EDGE('',*,*,#11425,.F.);
#16365=ORIENTED_EDGE('',*,*,#11426,.F.);
#16366=ORIENTED_EDGE('',*,*,#11427,.F.);
#16367=ORIENTED_EDGE('',*,*,#11428,.F.);
#16368=ORIENTED_EDGE('',*,*,#11429,.F.);
#16369=ORIENTED_EDGE('',*,*,#11430,.F.);
#16370=ORIENTED_EDGE('',*,*,#11431,.F.);
#16371=ORIENTED_EDGE('',*,*,#11432,.F.);
#16372=ORIENTED_EDGE('',*,*,#11433,.F.);
#16373=ORIENTED_EDGE('',*,*,#11434,.F.);
#16374=ORIENTED_EDGE('',*,*,#11435,.F.);
#16375=ORIENTED_EDGE('',*,*,#11436,.F.);
#16376=ORIENTED_EDGE('',*,*,#11437,.F.);
#16377=ORIENTED_EDGE('',*,*,#11438,.F.);
#16378=ORIENTED_EDGE('',*,*,#11439,.F.);
#16379=ORIENTED_EDGE('',*,*,#11440,.F.);
#16380=ORIENTED_EDGE('',*,*,#11441,.F.);
#16381=ORIENTED_EDGE('',*,*,#11442,.F.);
#16382=ORIENTED_EDGE('',*,*,#11443,.F.);
#16383=ORIENTED_EDGE('',*,*,#11444,.F.);
#16384=ORIENTED_EDGE('',*,*,#11445,.F.);
#16385=ORIENTED_EDGE('',*,*,#11446,.F.);
#16386=ORIENTED_EDGE('',*,*,#11447,.F.);
#16387=ORIENTED_EDGE('',*,*,#11448,.F.);
#16388=ORIENTED_EDGE('',*,*,#11449,.F.);
#16389=ORIENTED_EDGE('',*,*,#11450,.F.);
#16390=ORIENTED_EDGE('',*,*,#11451,.F.);
#16391=ORIENTED_EDGE('',*,*,#11452,.F.);
#16392=ORIENTED_EDGE('',*,*,#11453,.F.);
#16393=ORIENTED_EDGE('',*,*,#11454,.F.);
#16394=ORIENTED_EDGE('',*,*,#11455,.F.);
#16395=ORIENTED_EDGE('',*,*,#11456,.F.);
#16396=ORIENTED_EDGE('',*,*,#11457,.F.);
#16397=ORIENTED_EDGE('',*,*,#11458,.F.);
#16398=ORIENTED_EDGE('',*,*,#11459,.F.);
#16399=ORIENTED_EDGE('',*,*,#11460,.F.);
#16400=ORIENTED_EDGE('',*,*,#11461,.F.);
#16401=ORIENTED_EDGE('',*,*,#11462,.F.);
#16402=ORIENTED_EDGE('',*,*,#11463,.F.);
#16403=ORIENTED_EDGE('',*,*,#11464,.F.);
#16404=ORIENTED_EDGE('',*,*,#11465,.F.);
#16405=ORIENTED_EDGE('',*,*,#11466,.F.);
#16406=ORIENTED_EDGE('',*,*,#11467,.F.);
#16407=ORIENTED_EDGE('',*,*,#11468,.F.);
#16408=ORIENTED_EDGE('',*,*,#11469,.F.);
#16409=ORIENTED_EDGE('',*,*,#11470,.F.);
#16410=ORIENTED_EDGE('',*,*,#11471,.F.);
#16411=ORIENTED_EDGE('',*,*,#11472,.F.);
#16412=ORIENTED_EDGE('',*,*,#11473,.F.);
#16413=ORIENTED_EDGE('',*,*,#11474,.F.);
#16414=ORIENTED_EDGE('',*,*,#11475,.F.);
#16415=ORIENTED_EDGE('',*,*,#11476,.F.);
#16416=ORIENTED_EDGE('',*,*,#11477,.F.);
#16417=ORIENTED_EDGE('',*,*,#11478,.F.);
#16418=ORIENTED_EDGE('',*,*,#11479,.F.);
#16419=ORIENTED_EDGE('',*,*,#11480,.F.);
#16420=ORIENTED_EDGE('',*,*,#11481,.F.);
#16421=ORIENTED_EDGE('',*,*,#11482,.F.);
#16422=ORIENTED_EDGE('',*,*,#11483,.F.);
#16423=ORIENTED_EDGE('',*,*,#11484,.F.);
#16424=ORIENTED_EDGE('',*,*,#11485,.F.);
#16425=ORIENTED_EDGE('',*,*,#11486,.F.);
#16426=ORIENTED_EDGE('',*,*,#11487,.F.);
#16427=ORIENTED_EDGE('',*,*,#11488,.F.);
#16428=ORIENTED_EDGE('',*,*,#11489,.F.);
#16429=ORIENTED_EDGE('',*,*,#11490,.F.);
#16430=ORIENTED_EDGE('',*,*,#11491,.F.);
#16431=ORIENTED_EDGE('',*,*,#11492,.F.);
#16432=ORIENTED_EDGE('',*,*,#11493,.F.);
#16433=ORIENTED_EDGE('',*,*,#11494,.F.);
#16434=ORIENTED_EDGE('',*,*,#11495,.F.);
#16435=ORIENTED_EDGE('',*,*,#11496,.F.);
#16436=ORIENTED_EDGE('',*,*,#11497,.F.);
#16437=ORIENTED_EDGE('',*,*,#11498,.F.);
#16438=ORIENTED_EDGE('',*,*,#11499,.F.);
#16439=ORIENTED_EDGE('',*,*,#11500,.F.);
#16440=ORIENTED_EDGE('',*,*,#11501,.F.);
#16441=ORIENTED_EDGE('',*,*,#11502,.F.);
#16442=ORIENTED_EDGE('',*,*,#11503,.F.);
#16443=ORIENTED_EDGE('',*,*,#11504,.F.);
#16444=ORIENTED_EDGE('',*,*,#11505,.F.);
#16445=ORIENTED_EDGE('',*,*,#11506,.F.);
#16446=ORIENTED_EDGE('',*,*,#11351,.F.);
#16447=ORIENTED_EDGE('',*,*,#11507,.T.);
#16448=ORIENTED_EDGE('',*,*,#11508,.T.);
#16449=ORIENTED_EDGE('',*,*,#11355,.T.);
#16450=ORIENTED_EDGE('',*,*,#11508,.F.);
#16451=ORIENTED_EDGE('',*,*,#11509,.T.);
#16452=ORIENTED_EDGE('',*,*,#11510,.T.);
#16453=ORIENTED_EDGE('',*,*,#11511,.T.);
#16454=ORIENTED_EDGE('',*,*,#11512,.T.);
#16455=ORIENTED_EDGE('',*,*,#11513,.T.);
#16456=ORIENTED_EDGE('',*,*,#11514,.T.);
#16457=ORIENTED_EDGE('',*,*,#11515,.T.);
#16458=ORIENTED_EDGE('',*,*,#11516,.T.);
#16459=ORIENTED_EDGE('',*,*,#11517,.T.);
#16460=ORIENTED_EDGE('',*,*,#11518,.T.);
#16461=ORIENTED_EDGE('',*,*,#11519,.T.);
#16462=ORIENTED_EDGE('',*,*,#11520,.T.);
#16463=ORIENTED_EDGE('',*,*,#11521,.T.);
#16464=ORIENTED_EDGE('',*,*,#11522,.T.);
#16465=ORIENTED_EDGE('',*,*,#11523,.T.);
#16466=ORIENTED_EDGE('',*,*,#11524,.T.);
#16467=ORIENTED_EDGE('',*,*,#11525,.T.);
#16468=ORIENTED_EDGE('',*,*,#11526,.T.);
#16469=ORIENTED_EDGE('',*,*,#11527,.T.);
#16470=ORIENTED_EDGE('',*,*,#11528,.T.);
#16471=ORIENTED_EDGE('',*,*,#11529,.T.);
#16472=ORIENTED_EDGE('',*,*,#11530,.T.);
#16473=ORIENTED_EDGE('',*,*,#11531,.T.);
#16474=ORIENTED_EDGE('',*,*,#11532,.T.);
#16475=ORIENTED_EDGE('',*,*,#11533,.T.);
#16476=ORIENTED_EDGE('',*,*,#11534,.T.);
#16477=ORIENTED_EDGE('',*,*,#11535,.T.);
#16478=ORIENTED_EDGE('',*,*,#11536,.T.);
#16479=ORIENTED_EDGE('',*,*,#11537,.T.);
#16480=ORIENTED_EDGE('',*,*,#11538,.T.);
#16481=ORIENTED_EDGE('',*,*,#11539,.T.);
#16482=ORIENTED_EDGE('',*,*,#11540,.T.);
#16483=ORIENTED_EDGE('',*,*,#11541,.T.);
#16484=ORIENTED_EDGE('',*,*,#11542,.T.);
#16485=ORIENTED_EDGE('',*,*,#11543,.T.);
#16486=ORIENTED_EDGE('',*,*,#11544,.T.);
#16487=ORIENTED_EDGE('',*,*,#11545,.T.);
#16488=ORIENTED_EDGE('',*,*,#11546,.T.);
#16489=ORIENTED_EDGE('',*,*,#11547,.T.);
#16490=ORIENTED_EDGE('',*,*,#11548,.T.);
#16491=ORIENTED_EDGE('',*,*,#11549,.T.);
#16492=ORIENTED_EDGE('',*,*,#11550,.T.);
#16493=ORIENTED_EDGE('',*,*,#11551,.T.);
#16494=ORIENTED_EDGE('',*,*,#11552,.T.);
#16495=ORIENTED_EDGE('',*,*,#11553,.T.);
#16496=ORIENTED_EDGE('',*,*,#11554,.T.);
#16497=ORIENTED_EDGE('',*,*,#11555,.T.);
#16498=ORIENTED_EDGE('',*,*,#11556,.T.);
#16499=ORIENTED_EDGE('',*,*,#11557,.T.);
#16500=ORIENTED_EDGE('',*,*,#11558,.T.);
#16501=ORIENTED_EDGE('',*,*,#11559,.T.);
#16502=ORIENTED_EDGE('',*,*,#11560,.T.);
#16503=ORIENTED_EDGE('',*,*,#11561,.T.);
#16504=ORIENTED_EDGE('',*,*,#11562,.T.);
#16505=ORIENTED_EDGE('',*,*,#11563,.T.);
#16506=ORIENTED_EDGE('',*,*,#11564,.T.);
#16507=ORIENTED_EDGE('',*,*,#11565,.T.);
#16508=ORIENTED_EDGE('',*,*,#11566,.T.);
#16509=ORIENTED_EDGE('',*,*,#11567,.T.);
#16510=ORIENTED_EDGE('',*,*,#11568,.T.);
#16511=ORIENTED_EDGE('',*,*,#11569,.T.);
#16512=ORIENTED_EDGE('',*,*,#11570,.T.);
#16513=ORIENTED_EDGE('',*,*,#11571,.T.);
#16514=ORIENTED_EDGE('',*,*,#11572,.T.);
#16515=ORIENTED_EDGE('',*,*,#11573,.T.);
#16516=ORIENTED_EDGE('',*,*,#11574,.T.);
#16517=ORIENTED_EDGE('',*,*,#11575,.T.);
#16518=ORIENTED_EDGE('',*,*,#11576,.T.);
#16519=ORIENTED_EDGE('',*,*,#11577,.T.);
#16520=ORIENTED_EDGE('',*,*,#11578,.T.);
#16521=ORIENTED_EDGE('',*,*,#11579,.T.);
#16522=ORIENTED_EDGE('',*,*,#11580,.T.);
#16523=ORIENTED_EDGE('',*,*,#11581,.T.);
#16524=ORIENTED_EDGE('',*,*,#11582,.T.);
#16525=ORIENTED_EDGE('',*,*,#11583,.T.);
#16526=ORIENTED_EDGE('',*,*,#11584,.T.);
#16527=ORIENTED_EDGE('',*,*,#11585,.T.);
#16528=ORIENTED_EDGE('',*,*,#11586,.T.);
#16529=ORIENTED_EDGE('',*,*,#11587,.T.);
#16530=ORIENTED_EDGE('',*,*,#11588,.T.);
#16531=ORIENTED_EDGE('',*,*,#11589,.T.);
#16532=ORIENTED_EDGE('',*,*,#11590,.T.);
#16533=ORIENTED_EDGE('',*,*,#11591,.T.);
#16534=ORIENTED_EDGE('',*,*,#11592,.T.);
#16535=ORIENTED_EDGE('',*,*,#11593,.T.);
#16536=ORIENTED_EDGE('',*,*,#11594,.T.);
#16537=ORIENTED_EDGE('',*,*,#11595,.T.);
#16538=ORIENTED_EDGE('',*,*,#11596,.T.);
#16539=ORIENTED_EDGE('',*,*,#11597,.T.);
#16540=ORIENTED_EDGE('',*,*,#11598,.T.);
#16541=ORIENTED_EDGE('',*,*,#11599,.T.);
#16542=ORIENTED_EDGE('',*,*,#11600,.T.);
#16543=ORIENTED_EDGE('',*,*,#11601,.T.);
#16544=ORIENTED_EDGE('',*,*,#11602,.T.);
#16545=ORIENTED_EDGE('',*,*,#11603,.T.);
#16546=ORIENTED_EDGE('',*,*,#11604,.T.);
#16547=ORIENTED_EDGE('',*,*,#11605,.T.);
#16548=ORIENTED_EDGE('',*,*,#11606,.T.);
#16549=ORIENTED_EDGE('',*,*,#11607,.T.);
#16550=ORIENTED_EDGE('',*,*,#11608,.T.);
#16551=ORIENTED_EDGE('',*,*,#11609,.T.);
#16552=ORIENTED_EDGE('',*,*,#11610,.T.);
#16553=ORIENTED_EDGE('',*,*,#11611,.T.);
#16554=ORIENTED_EDGE('',*,*,#11612,.T.);
#16555=ORIENTED_EDGE('',*,*,#11613,.T.);
#16556=ORIENTED_EDGE('',*,*,#11614,.T.);
#16557=ORIENTED_EDGE('',*,*,#11615,.T.);
#16558=ORIENTED_EDGE('',*,*,#11616,.T.);
#16559=ORIENTED_EDGE('',*,*,#11617,.T.);
#16560=ORIENTED_EDGE('',*,*,#11618,.T.);
#16561=ORIENTED_EDGE('',*,*,#11619,.T.);
#16562=ORIENTED_EDGE('',*,*,#11620,.T.);
#16563=ORIENTED_EDGE('',*,*,#11621,.T.);
#16564=ORIENTED_EDGE('',*,*,#11622,.T.);
#16565=ORIENTED_EDGE('',*,*,#11623,.T.);
#16566=ORIENTED_EDGE('',*,*,#11624,.T.);
#16567=ORIENTED_EDGE('',*,*,#11625,.T.);
#16568=ORIENTED_EDGE('',*,*,#11626,.T.);
#16569=ORIENTED_EDGE('',*,*,#11627,.T.);
#16570=ORIENTED_EDGE('',*,*,#11628,.T.);
#16571=ORIENTED_EDGE('',*,*,#11629,.T.);
#16572=ORIENTED_EDGE('',*,*,#11630,.T.);
#16573=ORIENTED_EDGE('',*,*,#11631,.T.);
#16574=ORIENTED_EDGE('',*,*,#11632,.T.);
#16575=ORIENTED_EDGE('',*,*,#11633,.T.);
#16576=ORIENTED_EDGE('',*,*,#11634,.T.);
#16577=ORIENTED_EDGE('',*,*,#11635,.T.);
#16578=ORIENTED_EDGE('',*,*,#11636,.T.);
#16579=ORIENTED_EDGE('',*,*,#11637,.T.);
#16580=ORIENTED_EDGE('',*,*,#11638,.T.);
#16581=ORIENTED_EDGE('',*,*,#11639,.T.);
#16582=ORIENTED_EDGE('',*,*,#11640,.T.);
#16583=ORIENTED_EDGE('',*,*,#11641,.T.);
#16584=ORIENTED_EDGE('',*,*,#11642,.T.);
#16585=ORIENTED_EDGE('',*,*,#11643,.T.);
#16586=ORIENTED_EDGE('',*,*,#11644,.T.);
#16587=ORIENTED_EDGE('',*,*,#11645,.T.);
#16588=ORIENTED_EDGE('',*,*,#11646,.T.);
#16589=ORIENTED_EDGE('',*,*,#11647,.T.);
#16590=ORIENTED_EDGE('',*,*,#11648,.T.);
#16591=ORIENTED_EDGE('',*,*,#11649,.T.);
#16592=ORIENTED_EDGE('',*,*,#11650,.T.);
#16593=ORIENTED_EDGE('',*,*,#11651,.T.);
#16594=ORIENTED_EDGE('',*,*,#11652,.T.);
#16595=ORIENTED_EDGE('',*,*,#11653,.T.);
#16596=ORIENTED_EDGE('',*,*,#11654,.T.);
#16597=ORIENTED_EDGE('',*,*,#11655,.T.);
#16598=ORIENTED_EDGE('',*,*,#11656,.T.);
#16599=ORIENTED_EDGE('',*,*,#11657,.T.);
#16600=ORIENTED_EDGE('',*,*,#11658,.T.);
#16601=ORIENTED_EDGE('',*,*,#11659,.F.);
#16602=ORIENTED_EDGE('',*,*,#11507,.F.);
#16603=ORIENTED_EDGE('',*,*,#11506,.T.);
#16604=ORIENTED_EDGE('',*,*,#11660,.T.);
#16605=ORIENTED_EDGE('',*,*,#11661,.T.);
#16606=ORIENTED_EDGE('',*,*,#11660,.F.);
#16607=ORIENTED_EDGE('',*,*,#11661,.F.);
#16608=ORIENTED_EDGE('',*,*,#11662,.T.);
#16609=ORIENTED_EDGE('',*,*,#11663,.F.);
#16610=ORIENTED_EDGE('',*,*,#11662,.F.);
#16611=ORIENTED_EDGE('',*,*,#11659,.T.);
#16612=ORIENTED_EDGE('',*,*,#11664,.T.);
#16613=ORIENTED_EDGE('',*,*,#11663,.T.);
#16614=ORIENTED_EDGE('',*,*,#11664,.F.);
#16615=ORIENTED_EDGE('',*,*,#11357,.T.);
#16616=ORIENTED_EDGE('',*,*,#11665,.T.);
#16617=ORIENTED_EDGE('',*,*,#11658,.F.);
#16618=ORIENTED_EDGE('',*,*,#11666,.F.);
#16619=ORIENTED_EDGE('',*,*,#11358,.T.);
#16620=ORIENTED_EDGE('',*,*,#11666,.T.);
#16621=ORIENTED_EDGE('',*,*,#11657,.F.);
#16622=ORIENTED_EDGE('',*,*,#11667,.F.);
#16623=ORIENTED_EDGE('',*,*,#11359,.T.);
#16624=ORIENTED_EDGE('',*,*,#11667,.T.);
#16625=ORIENTED_EDGE('',*,*,#11656,.F.);
#16626=ORIENTED_EDGE('',*,*,#11668,.F.);
#16627=ORIENTED_EDGE('',*,*,#11360,.T.);
#16628=ORIENTED_EDGE('',*,*,#11668,.T.);
#16629=ORIENTED_EDGE('',*,*,#11655,.F.);
#16630=ORIENTED_EDGE('',*,*,#11669,.F.);
#16631=ORIENTED_EDGE('',*,*,#11361,.T.);
#16632=ORIENTED_EDGE('',*,*,#11669,.T.);
#16633=ORIENTED_EDGE('',*,*,#11654,.F.);
#16634=ORIENTED_EDGE('',*,*,#11670,.F.);
#16635=ORIENTED_EDGE('',*,*,#11362,.T.);
#16636=ORIENTED_EDGE('',*,*,#11670,.T.);
#16637=ORIENTED_EDGE('',*,*,#11653,.F.);
#16638=ORIENTED_EDGE('',*,*,#11671,.F.);
#16639=ORIENTED_EDGE('',*,*,#11363,.T.);
#16640=ORIENTED_EDGE('',*,*,#11671,.T.);
#16641=ORIENTED_EDGE('',*,*,#11652,.F.);
#16642=ORIENTED_EDGE('',*,*,#11672,.F.);
#16643=ORIENTED_EDGE('',*,*,#11364,.T.);
#16644=ORIENTED_EDGE('',*,*,#11672,.T.);
#16645=ORIENTED_EDGE('',*,*,#11651,.F.);
#16646=ORIENTED_EDGE('',*,*,#11673,.F.);
#16647=ORIENTED_EDGE('',*,*,#11365,.T.);
#16648=ORIENTED_EDGE('',*,*,#11673,.T.);
#16649=ORIENTED_EDGE('',*,*,#11650,.F.);
#16650=ORIENTED_EDGE('',*,*,#11674,.F.);
#16651=ORIENTED_EDGE('',*,*,#11366,.T.);
#16652=ORIENTED_EDGE('',*,*,#11674,.T.);
#16653=ORIENTED_EDGE('',*,*,#11649,.F.);
#16654=ORIENTED_EDGE('',*,*,#11675,.F.);
#16655=ORIENTED_EDGE('',*,*,#11367,.T.);
#16656=ORIENTED_EDGE('',*,*,#11675,.T.);
#16657=ORIENTED_EDGE('',*,*,#11648,.F.);
#16658=ORIENTED_EDGE('',*,*,#11676,.F.);
#16659=ORIENTED_EDGE('',*,*,#11368,.T.);
#16660=ORIENTED_EDGE('',*,*,#11676,.T.);
#16661=ORIENTED_EDGE('',*,*,#11647,.F.);
#16662=ORIENTED_EDGE('',*,*,#11677,.F.);
#16663=ORIENTED_EDGE('',*,*,#11369,.T.);
#16664=ORIENTED_EDGE('',*,*,#11677,.T.);
#16665=ORIENTED_EDGE('',*,*,#11646,.F.);
#16666=ORIENTED_EDGE('',*,*,#11678,.F.);
#16667=ORIENTED_EDGE('',*,*,#11370,.T.);
#16668=ORIENTED_EDGE('',*,*,#11678,.T.);
#16669=ORIENTED_EDGE('',*,*,#11645,.F.);
#16670=ORIENTED_EDGE('',*,*,#11679,.F.);
#16671=ORIENTED_EDGE('',*,*,#11371,.T.);
#16672=ORIENTED_EDGE('',*,*,#11679,.T.);
#16673=ORIENTED_EDGE('',*,*,#11644,.F.);
#16674=ORIENTED_EDGE('',*,*,#11680,.F.);
#16675=ORIENTED_EDGE('',*,*,#11372,.T.);
#16676=ORIENTED_EDGE('',*,*,#11680,.T.);
#16677=ORIENTED_EDGE('',*,*,#11643,.F.);
#16678=ORIENTED_EDGE('',*,*,#11681,.F.);
#16679=ORIENTED_EDGE('',*,*,#11373,.T.);
#16680=ORIENTED_EDGE('',*,*,#11681,.T.);
#16681=ORIENTED_EDGE('',*,*,#11642,.F.);
#16682=ORIENTED_EDGE('',*,*,#11682,.F.);
#16683=ORIENTED_EDGE('',*,*,#11374,.T.);
#16684=ORIENTED_EDGE('',*,*,#11682,.T.);
#16685=ORIENTED_EDGE('',*,*,#11641,.F.);
#16686=ORIENTED_EDGE('',*,*,#11683,.F.);
#16687=ORIENTED_EDGE('',*,*,#11375,.T.);
#16688=ORIENTED_EDGE('',*,*,#11683,.T.);
#16689=ORIENTED_EDGE('',*,*,#11640,.F.);
#16690=ORIENTED_EDGE('',*,*,#11684,.F.);
#16691=ORIENTED_EDGE('',*,*,#11376,.T.);
#16692=ORIENTED_EDGE('',*,*,#11684,.T.);
#16693=ORIENTED_EDGE('',*,*,#11639,.F.);
#16694=ORIENTED_EDGE('',*,*,#11685,.F.);
#16695=ORIENTED_EDGE('',*,*,#11377,.T.);
#16696=ORIENTED_EDGE('',*,*,#11685,.T.);
#16697=ORIENTED_EDGE('',*,*,#11638,.F.);
#16698=ORIENTED_EDGE('',*,*,#11686,.F.);
#16699=ORIENTED_EDGE('',*,*,#11378,.T.);
#16700=ORIENTED_EDGE('',*,*,#11686,.T.);
#16701=ORIENTED_EDGE('',*,*,#11637,.F.);
#16702=ORIENTED_EDGE('',*,*,#11687,.F.);
#16703=ORIENTED_EDGE('',*,*,#11379,.T.);
#16704=ORIENTED_EDGE('',*,*,#11687,.T.);
#16705=ORIENTED_EDGE('',*,*,#11636,.F.);
#16706=ORIENTED_EDGE('',*,*,#11688,.F.);
#16707=ORIENTED_EDGE('',*,*,#11380,.T.);
#16708=ORIENTED_EDGE('',*,*,#11688,.T.);
#16709=ORIENTED_EDGE('',*,*,#11635,.F.);
#16710=ORIENTED_EDGE('',*,*,#11689,.F.);
#16711=ORIENTED_EDGE('',*,*,#11381,.T.);
#16712=ORIENTED_EDGE('',*,*,#11689,.T.);
#16713=ORIENTED_EDGE('',*,*,#11634,.F.);
#16714=ORIENTED_EDGE('',*,*,#11690,.F.);
#16715=ORIENTED_EDGE('',*,*,#11382,.T.);
#16716=ORIENTED_EDGE('',*,*,#11690,.T.);
#16717=ORIENTED_EDGE('',*,*,#11633,.F.);
#16718=ORIENTED_EDGE('',*,*,#11691,.F.);
#16719=ORIENTED_EDGE('',*,*,#11383,.T.);
#16720=ORIENTED_EDGE('',*,*,#11691,.T.);
#16721=ORIENTED_EDGE('',*,*,#11632,.F.);
#16722=ORIENTED_EDGE('',*,*,#11692,.F.);
#16723=ORIENTED_EDGE('',*,*,#11384,.T.);
#16724=ORIENTED_EDGE('',*,*,#11692,.T.);
#16725=ORIENTED_EDGE('',*,*,#11631,.F.);
#16726=ORIENTED_EDGE('',*,*,#11693,.F.);
#16727=ORIENTED_EDGE('',*,*,#11385,.T.);
#16728=ORIENTED_EDGE('',*,*,#11693,.T.);
#16729=ORIENTED_EDGE('',*,*,#11630,.F.);
#16730=ORIENTED_EDGE('',*,*,#11694,.F.);
#16731=ORIENTED_EDGE('',*,*,#11386,.T.);
#16732=ORIENTED_EDGE('',*,*,#11694,.T.);
#16733=ORIENTED_EDGE('',*,*,#11629,.F.);
#16734=ORIENTED_EDGE('',*,*,#11695,.F.);
#16735=ORIENTED_EDGE('',*,*,#11387,.T.);
#16736=ORIENTED_EDGE('',*,*,#11695,.T.);
#16737=ORIENTED_EDGE('',*,*,#11628,.F.);
#16738=ORIENTED_EDGE('',*,*,#11696,.F.);
#16739=ORIENTED_EDGE('',*,*,#11388,.T.);
#16740=ORIENTED_EDGE('',*,*,#11696,.T.);
#16741=ORIENTED_EDGE('',*,*,#11627,.F.);
#16742=ORIENTED_EDGE('',*,*,#11697,.F.);
#16743=ORIENTED_EDGE('',*,*,#11389,.T.);
#16744=ORIENTED_EDGE('',*,*,#11697,.T.);
#16745=ORIENTED_EDGE('',*,*,#11626,.F.);
#16746=ORIENTED_EDGE('',*,*,#11698,.F.);
#16747=ORIENTED_EDGE('',*,*,#11390,.T.);
#16748=ORIENTED_EDGE('',*,*,#11698,.T.);
#16749=ORIENTED_EDGE('',*,*,#11625,.F.);
#16750=ORIENTED_EDGE('',*,*,#11699,.F.);
#16751=ORIENTED_EDGE('',*,*,#11391,.T.);
#16752=ORIENTED_EDGE('',*,*,#11699,.T.);
#16753=ORIENTED_EDGE('',*,*,#11624,.F.);
#16754=ORIENTED_EDGE('',*,*,#11700,.F.);
#16755=ORIENTED_EDGE('',*,*,#11392,.T.);
#16756=ORIENTED_EDGE('',*,*,#11700,.T.);
#16757=ORIENTED_EDGE('',*,*,#11623,.F.);
#16758=ORIENTED_EDGE('',*,*,#11701,.F.);
#16759=ORIENTED_EDGE('',*,*,#11393,.T.);
#16760=ORIENTED_EDGE('',*,*,#11701,.T.);
#16761=ORIENTED_EDGE('',*,*,#11622,.F.);
#16762=ORIENTED_EDGE('',*,*,#11702,.F.);
#16763=ORIENTED_EDGE('',*,*,#11394,.T.);
#16764=ORIENTED_EDGE('',*,*,#11702,.T.);
#16765=ORIENTED_EDGE('',*,*,#11621,.F.);
#16766=ORIENTED_EDGE('',*,*,#11703,.F.);
#16767=ORIENTED_EDGE('',*,*,#11395,.T.);
#16768=ORIENTED_EDGE('',*,*,#11703,.T.);
#16769=ORIENTED_EDGE('',*,*,#11620,.F.);
#16770=ORIENTED_EDGE('',*,*,#11704,.F.);
#16771=ORIENTED_EDGE('',*,*,#11396,.T.);
#16772=ORIENTED_EDGE('',*,*,#11704,.T.);
#16773=ORIENTED_EDGE('',*,*,#11619,.F.);
#16774=ORIENTED_EDGE('',*,*,#11705,.F.);
#16775=ORIENTED_EDGE('',*,*,#11397,.T.);
#16776=ORIENTED_EDGE('',*,*,#11705,.T.);
#16777=ORIENTED_EDGE('',*,*,#11618,.F.);
#16778=ORIENTED_EDGE('',*,*,#11706,.F.);
#16779=ORIENTED_EDGE('',*,*,#11398,.T.);
#16780=ORIENTED_EDGE('',*,*,#11706,.T.);
#16781=ORIENTED_EDGE('',*,*,#11617,.F.);
#16782=ORIENTED_EDGE('',*,*,#11707,.F.);
#16783=ORIENTED_EDGE('',*,*,#11399,.T.);
#16784=ORIENTED_EDGE('',*,*,#11707,.T.);
#16785=ORIENTED_EDGE('',*,*,#11616,.F.);
#16786=ORIENTED_EDGE('',*,*,#11708,.F.);
#16787=ORIENTED_EDGE('',*,*,#11400,.T.);
#16788=ORIENTED_EDGE('',*,*,#11708,.T.);
#16789=ORIENTED_EDGE('',*,*,#11615,.F.);
#16790=ORIENTED_EDGE('',*,*,#11709,.F.);
#16791=ORIENTED_EDGE('',*,*,#11401,.T.);
#16792=ORIENTED_EDGE('',*,*,#11709,.T.);
#16793=ORIENTED_EDGE('',*,*,#11614,.F.);
#16794=ORIENTED_EDGE('',*,*,#11710,.F.);
#16795=ORIENTED_EDGE('',*,*,#11402,.T.);
#16796=ORIENTED_EDGE('',*,*,#11710,.T.);
#16797=ORIENTED_EDGE('',*,*,#11613,.F.);
#16798=ORIENTED_EDGE('',*,*,#11711,.F.);
#16799=ORIENTED_EDGE('',*,*,#11403,.T.);
#16800=ORIENTED_EDGE('',*,*,#11711,.T.);
#16801=ORIENTED_EDGE('',*,*,#11612,.F.);
#16802=ORIENTED_EDGE('',*,*,#11712,.F.);
#16803=ORIENTED_EDGE('',*,*,#11404,.T.);
#16804=ORIENTED_EDGE('',*,*,#11712,.T.);
#16805=ORIENTED_EDGE('',*,*,#11611,.F.);
#16806=ORIENTED_EDGE('',*,*,#11713,.F.);
#16807=ORIENTED_EDGE('',*,*,#11405,.T.);
#16808=ORIENTED_EDGE('',*,*,#11713,.T.);
#16809=ORIENTED_EDGE('',*,*,#11610,.F.);
#16810=ORIENTED_EDGE('',*,*,#11714,.F.);
#16811=ORIENTED_EDGE('',*,*,#11406,.T.);
#16812=ORIENTED_EDGE('',*,*,#11714,.T.);
#16813=ORIENTED_EDGE('',*,*,#11609,.F.);
#16814=ORIENTED_EDGE('',*,*,#11715,.F.);
#16815=ORIENTED_EDGE('',*,*,#11407,.T.);
#16816=ORIENTED_EDGE('',*,*,#11715,.T.);
#16817=ORIENTED_EDGE('',*,*,#11608,.F.);
#16818=ORIENTED_EDGE('',*,*,#11716,.F.);
#16819=ORIENTED_EDGE('',*,*,#11408,.T.);
#16820=ORIENTED_EDGE('',*,*,#11716,.T.);
#16821=ORIENTED_EDGE('',*,*,#11607,.F.);
#16822=ORIENTED_EDGE('',*,*,#11717,.F.);
#16823=ORIENTED_EDGE('',*,*,#11409,.T.);
#16824=ORIENTED_EDGE('',*,*,#11717,.T.);
#16825=ORIENTED_EDGE('',*,*,#11606,.F.);
#16826=ORIENTED_EDGE('',*,*,#11718,.F.);
#16827=ORIENTED_EDGE('',*,*,#11410,.T.);
#16828=ORIENTED_EDGE('',*,*,#11718,.T.);
#16829=ORIENTED_EDGE('',*,*,#11605,.F.);
#16830=ORIENTED_EDGE('',*,*,#11719,.F.);
#16831=ORIENTED_EDGE('',*,*,#11411,.T.);
#16832=ORIENTED_EDGE('',*,*,#11719,.T.);
#16833=ORIENTED_EDGE('',*,*,#11604,.F.);
#16834=ORIENTED_EDGE('',*,*,#11720,.F.);
#16835=ORIENTED_EDGE('',*,*,#11412,.T.);
#16836=ORIENTED_EDGE('',*,*,#11720,.T.);
#16837=ORIENTED_EDGE('',*,*,#11603,.F.);
#16838=ORIENTED_EDGE('',*,*,#11721,.F.);
#16839=ORIENTED_EDGE('',*,*,#11413,.T.);
#16840=ORIENTED_EDGE('',*,*,#11721,.T.);
#16841=ORIENTED_EDGE('',*,*,#11602,.F.);
#16842=ORIENTED_EDGE('',*,*,#11722,.F.);
#16843=ORIENTED_EDGE('',*,*,#11414,.T.);
#16844=ORIENTED_EDGE('',*,*,#11722,.T.);
#16845=ORIENTED_EDGE('',*,*,#11601,.F.);
#16846=ORIENTED_EDGE('',*,*,#11723,.F.);
#16847=ORIENTED_EDGE('',*,*,#11415,.T.);
#16848=ORIENTED_EDGE('',*,*,#11723,.T.);
#16849=ORIENTED_EDGE('',*,*,#11600,.F.);
#16850=ORIENTED_EDGE('',*,*,#11724,.F.);
#16851=ORIENTED_EDGE('',*,*,#11416,.T.);
#16852=ORIENTED_EDGE('',*,*,#11724,.T.);
#16853=ORIENTED_EDGE('',*,*,#11599,.F.);
#16854=ORIENTED_EDGE('',*,*,#11725,.F.);
#16855=ORIENTED_EDGE('',*,*,#11417,.T.);
#16856=ORIENTED_EDGE('',*,*,#11725,.T.);
#16857=ORIENTED_EDGE('',*,*,#11598,.F.);
#16858=ORIENTED_EDGE('',*,*,#11726,.F.);
#16859=ORIENTED_EDGE('',*,*,#11418,.T.);
#16860=ORIENTED_EDGE('',*,*,#11726,.T.);
#16861=ORIENTED_EDGE('',*,*,#11597,.F.);
#16862=ORIENTED_EDGE('',*,*,#11727,.F.);
#16863=ORIENTED_EDGE('',*,*,#11419,.T.);
#16864=ORIENTED_EDGE('',*,*,#11727,.T.);
#16865=ORIENTED_EDGE('',*,*,#11596,.F.);
#16866=ORIENTED_EDGE('',*,*,#11728,.F.);
#16867=ORIENTED_EDGE('',*,*,#11420,.T.);
#16868=ORIENTED_EDGE('',*,*,#11728,.T.);
#16869=ORIENTED_EDGE('',*,*,#11595,.F.);
#16870=ORIENTED_EDGE('',*,*,#11729,.F.);
#16871=ORIENTED_EDGE('',*,*,#11421,.T.);
#16872=ORIENTED_EDGE('',*,*,#11729,.T.);
#16873=ORIENTED_EDGE('',*,*,#11594,.F.);
#16874=ORIENTED_EDGE('',*,*,#11730,.F.);
#16875=ORIENTED_EDGE('',*,*,#11422,.T.);
#16876=ORIENTED_EDGE('',*,*,#11730,.T.);
#16877=ORIENTED_EDGE('',*,*,#11593,.F.);
#16878=ORIENTED_EDGE('',*,*,#11731,.F.);
#16879=ORIENTED_EDGE('',*,*,#11423,.T.);
#16880=ORIENTED_EDGE('',*,*,#11731,.T.);
#16881=ORIENTED_EDGE('',*,*,#11592,.F.);
#16882=ORIENTED_EDGE('',*,*,#11732,.F.);
#16883=ORIENTED_EDGE('',*,*,#11424,.T.);
#16884=ORIENTED_EDGE('',*,*,#11732,.T.);
#16885=ORIENTED_EDGE('',*,*,#11591,.F.);
#16886=ORIENTED_EDGE('',*,*,#11733,.F.);
#16887=ORIENTED_EDGE('',*,*,#11425,.T.);
#16888=ORIENTED_EDGE('',*,*,#11733,.T.);
#16889=ORIENTED_EDGE('',*,*,#11590,.F.);
#16890=ORIENTED_EDGE('',*,*,#11734,.F.);
#16891=ORIENTED_EDGE('',*,*,#11426,.T.);
#16892=ORIENTED_EDGE('',*,*,#11734,.T.);
#16893=ORIENTED_EDGE('',*,*,#11589,.F.);
#16894=ORIENTED_EDGE('',*,*,#11735,.F.);
#16895=ORIENTED_EDGE('',*,*,#11427,.T.);
#16896=ORIENTED_EDGE('',*,*,#11735,.T.);
#16897=ORIENTED_EDGE('',*,*,#11588,.F.);
#16898=ORIENTED_EDGE('',*,*,#11736,.F.);
#16899=ORIENTED_EDGE('',*,*,#11428,.T.);
#16900=ORIENTED_EDGE('',*,*,#11736,.T.);
#16901=ORIENTED_EDGE('',*,*,#11587,.F.);
#16902=ORIENTED_EDGE('',*,*,#11737,.F.);
#16903=ORIENTED_EDGE('',*,*,#11429,.T.);
#16904=ORIENTED_EDGE('',*,*,#11737,.T.);
#16905=ORIENTED_EDGE('',*,*,#11586,.F.);
#16906=ORIENTED_EDGE('',*,*,#11738,.F.);
#16907=ORIENTED_EDGE('',*,*,#11430,.T.);
#16908=ORIENTED_EDGE('',*,*,#11738,.T.);
#16909=ORIENTED_EDGE('',*,*,#11585,.F.);
#16910=ORIENTED_EDGE('',*,*,#11739,.F.);
#16911=ORIENTED_EDGE('',*,*,#11431,.T.);
#16912=ORIENTED_EDGE('',*,*,#11739,.T.);
#16913=ORIENTED_EDGE('',*,*,#11584,.F.);
#16914=ORIENTED_EDGE('',*,*,#11740,.F.);
#16915=ORIENTED_EDGE('',*,*,#11432,.T.);
#16916=ORIENTED_EDGE('',*,*,#11740,.T.);
#16917=ORIENTED_EDGE('',*,*,#11583,.F.);
#16918=ORIENTED_EDGE('',*,*,#11741,.F.);
#16919=ORIENTED_EDGE('',*,*,#11433,.T.);
#16920=ORIENTED_EDGE('',*,*,#11741,.T.);
#16921=ORIENTED_EDGE('',*,*,#11582,.F.);
#16922=ORIENTED_EDGE('',*,*,#11742,.F.);
#16923=ORIENTED_EDGE('',*,*,#11434,.T.);
#16924=ORIENTED_EDGE('',*,*,#11742,.T.);
#16925=ORIENTED_EDGE('',*,*,#11581,.F.);
#16926=ORIENTED_EDGE('',*,*,#11743,.F.);
#16927=ORIENTED_EDGE('',*,*,#11435,.T.);
#16928=ORIENTED_EDGE('',*,*,#11743,.T.);
#16929=ORIENTED_EDGE('',*,*,#11580,.F.);
#16930=ORIENTED_EDGE('',*,*,#11744,.F.);
#16931=ORIENTED_EDGE('',*,*,#11436,.T.);
#16932=ORIENTED_EDGE('',*,*,#11744,.T.);
#16933=ORIENTED_EDGE('',*,*,#11579,.F.);
#16934=ORIENTED_EDGE('',*,*,#11745,.F.);
#16935=ORIENTED_EDGE('',*,*,#11437,.T.);
#16936=ORIENTED_EDGE('',*,*,#11745,.T.);
#16937=ORIENTED_EDGE('',*,*,#11578,.F.);
#16938=ORIENTED_EDGE('',*,*,#11746,.F.);
#16939=ORIENTED_EDGE('',*,*,#11438,.T.);
#16940=ORIENTED_EDGE('',*,*,#11746,.T.);
#16941=ORIENTED_EDGE('',*,*,#11577,.F.);
#16942=ORIENTED_EDGE('',*,*,#11747,.F.);
#16943=ORIENTED_EDGE('',*,*,#11439,.T.);
#16944=ORIENTED_EDGE('',*,*,#11747,.T.);
#16945=ORIENTED_EDGE('',*,*,#11576,.F.);
#16946=ORIENTED_EDGE('',*,*,#11748,.F.);
#16947=ORIENTED_EDGE('',*,*,#11440,.T.);
#16948=ORIENTED_EDGE('',*,*,#11748,.T.);
#16949=ORIENTED_EDGE('',*,*,#11575,.F.);
#16950=ORIENTED_EDGE('',*,*,#11749,.F.);
#16951=ORIENTED_EDGE('',*,*,#11441,.T.);
#16952=ORIENTED_EDGE('',*,*,#11749,.T.);
#16953=ORIENTED_EDGE('',*,*,#11574,.F.);
#16954=ORIENTED_EDGE('',*,*,#11750,.F.);
#16955=ORIENTED_EDGE('',*,*,#11442,.T.);
#16956=ORIENTED_EDGE('',*,*,#11750,.T.);
#16957=ORIENTED_EDGE('',*,*,#11573,.F.);
#16958=ORIENTED_EDGE('',*,*,#11751,.F.);
#16959=ORIENTED_EDGE('',*,*,#11443,.T.);
#16960=ORIENTED_EDGE('',*,*,#11751,.T.);
#16961=ORIENTED_EDGE('',*,*,#11572,.F.);
#16962=ORIENTED_EDGE('',*,*,#11752,.F.);
#16963=ORIENTED_EDGE('',*,*,#11444,.T.);
#16964=ORIENTED_EDGE('',*,*,#11752,.T.);
#16965=ORIENTED_EDGE('',*,*,#11571,.F.);
#16966=ORIENTED_EDGE('',*,*,#11753,.F.);
#16967=ORIENTED_EDGE('',*,*,#11445,.T.);
#16968=ORIENTED_EDGE('',*,*,#11753,.T.);
#16969=ORIENTED_EDGE('',*,*,#11570,.F.);
#16970=ORIENTED_EDGE('',*,*,#11754,.F.);
#16971=ORIENTED_EDGE('',*,*,#11446,.T.);
#16972=ORIENTED_EDGE('',*,*,#11754,.T.);
#16973=ORIENTED_EDGE('',*,*,#11569,.F.);
#16974=ORIENTED_EDGE('',*,*,#11755,.F.);
#16975=ORIENTED_EDGE('',*,*,#11447,.T.);
#16976=ORIENTED_EDGE('',*,*,#11755,.T.);
#16977=ORIENTED_EDGE('',*,*,#11568,.F.);
#16978=ORIENTED_EDGE('',*,*,#11756,.F.);
#16979=ORIENTED_EDGE('',*,*,#11448,.T.);
#16980=ORIENTED_EDGE('',*,*,#11756,.T.);
#16981=ORIENTED_EDGE('',*,*,#11567,.F.);
#16982=ORIENTED_EDGE('',*,*,#11757,.F.);
#16983=ORIENTED_EDGE('',*,*,#11449,.T.);
#16984=ORIENTED_EDGE('',*,*,#11757,.T.);
#16985=ORIENTED_EDGE('',*,*,#11566,.F.);
#16986=ORIENTED_EDGE('',*,*,#11758,.F.);
#16987=ORIENTED_EDGE('',*,*,#11450,.T.);
#16988=ORIENTED_EDGE('',*,*,#11758,.T.);
#16989=ORIENTED_EDGE('',*,*,#11565,.F.);
#16990=ORIENTED_EDGE('',*,*,#11759,.F.);
#16991=ORIENTED_EDGE('',*,*,#11451,.T.);
#16992=ORIENTED_EDGE('',*,*,#11759,.T.);
#16993=ORIENTED_EDGE('',*,*,#11564,.F.);
#16994=ORIENTED_EDGE('',*,*,#11760,.F.);
#16995=ORIENTED_EDGE('',*,*,#11452,.T.);
#16996=ORIENTED_EDGE('',*,*,#11760,.T.);
#16997=ORIENTED_EDGE('',*,*,#11563,.F.);
#16998=ORIENTED_EDGE('',*,*,#11761,.F.);
#16999=ORIENTED_EDGE('',*,*,#11453,.T.);
#17000=ORIENTED_EDGE('',*,*,#11761,.T.);
#17001=ORIENTED_EDGE('',*,*,#11562,.F.);
#17002=ORIENTED_EDGE('',*,*,#11762,.F.);
#17003=ORIENTED_EDGE('',*,*,#11454,.T.);
#17004=ORIENTED_EDGE('',*,*,#11762,.T.);
#17005=ORIENTED_EDGE('',*,*,#11561,.F.);
#17006=ORIENTED_EDGE('',*,*,#11763,.F.);
#17007=ORIENTED_EDGE('',*,*,#11455,.T.);
#17008=ORIENTED_EDGE('',*,*,#11763,.T.);
#17009=ORIENTED_EDGE('',*,*,#11560,.F.);
#17010=ORIENTED_EDGE('',*,*,#11764,.F.);
#17011=ORIENTED_EDGE('',*,*,#11456,.T.);
#17012=ORIENTED_EDGE('',*,*,#11764,.T.);
#17013=ORIENTED_EDGE('',*,*,#11559,.F.);
#17014=ORIENTED_EDGE('',*,*,#11765,.F.);
#17015=ORIENTED_EDGE('',*,*,#11457,.T.);
#17016=ORIENTED_EDGE('',*,*,#11765,.T.);
#17017=ORIENTED_EDGE('',*,*,#11558,.F.);
#17018=ORIENTED_EDGE('',*,*,#11766,.F.);
#17019=ORIENTED_EDGE('',*,*,#11458,.T.);
#17020=ORIENTED_EDGE('',*,*,#11766,.T.);
#17021=ORIENTED_EDGE('',*,*,#11557,.F.);
#17022=ORIENTED_EDGE('',*,*,#11767,.F.);
#17023=ORIENTED_EDGE('',*,*,#11459,.T.);
#17024=ORIENTED_EDGE('',*,*,#11767,.T.);
#17025=ORIENTED_EDGE('',*,*,#11556,.F.);
#17026=ORIENTED_EDGE('',*,*,#11768,.F.);
#17027=ORIENTED_EDGE('',*,*,#11460,.T.);
#17028=ORIENTED_EDGE('',*,*,#11768,.T.);
#17029=ORIENTED_EDGE('',*,*,#11555,.F.);
#17030=ORIENTED_EDGE('',*,*,#11769,.F.);
#17031=ORIENTED_EDGE('',*,*,#11461,.T.);
#17032=ORIENTED_EDGE('',*,*,#11769,.T.);
#17033=ORIENTED_EDGE('',*,*,#11554,.F.);
#17034=ORIENTED_EDGE('',*,*,#11770,.F.);
#17035=ORIENTED_EDGE('',*,*,#11462,.T.);
#17036=ORIENTED_EDGE('',*,*,#11770,.T.);
#17037=ORIENTED_EDGE('',*,*,#11553,.F.);
#17038=ORIENTED_EDGE('',*,*,#11771,.F.);
#17039=ORIENTED_EDGE('',*,*,#11463,.T.);
#17040=ORIENTED_EDGE('',*,*,#11771,.T.);
#17041=ORIENTED_EDGE('',*,*,#11552,.F.);
#17042=ORIENTED_EDGE('',*,*,#11772,.F.);
#17043=ORIENTED_EDGE('',*,*,#11464,.T.);
#17044=ORIENTED_EDGE('',*,*,#11772,.T.);
#17045=ORIENTED_EDGE('',*,*,#11551,.F.);
#17046=ORIENTED_EDGE('',*,*,#11773,.F.);
#17047=ORIENTED_EDGE('',*,*,#11465,.T.);
#17048=ORIENTED_EDGE('',*,*,#11773,.T.);
#17049=ORIENTED_EDGE('',*,*,#11550,.F.);
#17050=ORIENTED_EDGE('',*,*,#11774,.F.);
#17051=ORIENTED_EDGE('',*,*,#11466,.T.);
#17052=ORIENTED_EDGE('',*,*,#11774,.T.);
#17053=ORIENTED_EDGE('',*,*,#11549,.F.);
#17054=ORIENTED_EDGE('',*,*,#11775,.F.);
#17055=ORIENTED_EDGE('',*,*,#11467,.T.);
#17056=ORIENTED_EDGE('',*,*,#11775,.T.);
#17057=ORIENTED_EDGE('',*,*,#11548,.F.);
#17058=ORIENTED_EDGE('',*,*,#11776,.F.);
#17059=ORIENTED_EDGE('',*,*,#11468,.T.);
#17060=ORIENTED_EDGE('',*,*,#11776,.T.);
#17061=ORIENTED_EDGE('',*,*,#11547,.F.);
#17062=ORIENTED_EDGE('',*,*,#11777,.F.);
#17063=ORIENTED_EDGE('',*,*,#11469,.T.);
#17064=ORIENTED_EDGE('',*,*,#11777,.T.);
#17065=ORIENTED_EDGE('',*,*,#11546,.F.);
#17066=ORIENTED_EDGE('',*,*,#11778,.F.);
#17067=ORIENTED_EDGE('',*,*,#11470,.T.);
#17068=ORIENTED_EDGE('',*,*,#11778,.T.);
#17069=ORIENTED_EDGE('',*,*,#11545,.F.);
#17070=ORIENTED_EDGE('',*,*,#11779,.F.);
#17071=ORIENTED_EDGE('',*,*,#11471,.T.);
#17072=ORIENTED_EDGE('',*,*,#11779,.T.);
#17073=ORIENTED_EDGE('',*,*,#11544,.F.);
#17074=ORIENTED_EDGE('',*,*,#11780,.F.);
#17075=ORIENTED_EDGE('',*,*,#11472,.T.);
#17076=ORIENTED_EDGE('',*,*,#11780,.T.);
#17077=ORIENTED_EDGE('',*,*,#11543,.F.);
#17078=ORIENTED_EDGE('',*,*,#11781,.F.);
#17079=ORIENTED_EDGE('',*,*,#11473,.T.);
#17080=ORIENTED_EDGE('',*,*,#11781,.T.);
#17081=ORIENTED_EDGE('',*,*,#11542,.F.);
#17082=ORIENTED_EDGE('',*,*,#11782,.F.);
#17083=ORIENTED_EDGE('',*,*,#11474,.T.);
#17084=ORIENTED_EDGE('',*,*,#11782,.T.);
#17085=ORIENTED_EDGE('',*,*,#11541,.F.);
#17086=ORIENTED_EDGE('',*,*,#11783,.F.);
#17087=ORIENTED_EDGE('',*,*,#11475,.T.);
#17088=ORIENTED_EDGE('',*,*,#11783,.T.);
#17089=ORIENTED_EDGE('',*,*,#11540,.F.);
#17090=ORIENTED_EDGE('',*,*,#11784,.F.);
#17091=ORIENTED_EDGE('',*,*,#11476,.T.);
#17092=ORIENTED_EDGE('',*,*,#11784,.T.);
#17093=ORIENTED_EDGE('',*,*,#11539,.F.);
#17094=ORIENTED_EDGE('',*,*,#11785,.F.);
#17095=ORIENTED_EDGE('',*,*,#11477,.T.);
#17096=ORIENTED_EDGE('',*,*,#11785,.T.);
#17097=ORIENTED_EDGE('',*,*,#11538,.F.);
#17098=ORIENTED_EDGE('',*,*,#11786,.F.);
#17099=ORIENTED_EDGE('',*,*,#11478,.T.);
#17100=ORIENTED_EDGE('',*,*,#11786,.T.);
#17101=ORIENTED_EDGE('',*,*,#11537,.F.);
#17102=ORIENTED_EDGE('',*,*,#11787,.F.);
#17103=ORIENTED_EDGE('',*,*,#11479,.T.);
#17104=ORIENTED_EDGE('',*,*,#11787,.T.);
#17105=ORIENTED_EDGE('',*,*,#11536,.F.);
#17106=ORIENTED_EDGE('',*,*,#11788,.F.);
#17107=ORIENTED_EDGE('',*,*,#11480,.T.);
#17108=ORIENTED_EDGE('',*,*,#11788,.T.);
#17109=ORIENTED_EDGE('',*,*,#11535,.F.);
#17110=ORIENTED_EDGE('',*,*,#11789,.F.);
#17111=ORIENTED_EDGE('',*,*,#11481,.T.);
#17112=ORIENTED_EDGE('',*,*,#11789,.T.);
#17113=ORIENTED_EDGE('',*,*,#11534,.F.);
#17114=ORIENTED_EDGE('',*,*,#11790,.F.);
#17115=ORIENTED_EDGE('',*,*,#11482,.T.);
#17116=ORIENTED_EDGE('',*,*,#11790,.T.);
#17117=ORIENTED_EDGE('',*,*,#11533,.F.);
#17118=ORIENTED_EDGE('',*,*,#11791,.F.);
#17119=ORIENTED_EDGE('',*,*,#11483,.T.);
#17120=ORIENTED_EDGE('',*,*,#11791,.T.);
#17121=ORIENTED_EDGE('',*,*,#11532,.F.);
#17122=ORIENTED_EDGE('',*,*,#11792,.F.);
#17123=ORIENTED_EDGE('',*,*,#11484,.T.);
#17124=ORIENTED_EDGE('',*,*,#11792,.T.);
#17125=ORIENTED_EDGE('',*,*,#11531,.F.);
#17126=ORIENTED_EDGE('',*,*,#11793,.F.);
#17127=ORIENTED_EDGE('',*,*,#11485,.T.);
#17128=ORIENTED_EDGE('',*,*,#11793,.T.);
#17129=ORIENTED_EDGE('',*,*,#11530,.F.);
#17130=ORIENTED_EDGE('',*,*,#11794,.F.);
#17131=ORIENTED_EDGE('',*,*,#11486,.T.);
#17132=ORIENTED_EDGE('',*,*,#11794,.T.);
#17133=ORIENTED_EDGE('',*,*,#11529,.F.);
#17134=ORIENTED_EDGE('',*,*,#11795,.F.);
#17135=ORIENTED_EDGE('',*,*,#11487,.T.);
#17136=ORIENTED_EDGE('',*,*,#11795,.T.);
#17137=ORIENTED_EDGE('',*,*,#11528,.F.);
#17138=ORIENTED_EDGE('',*,*,#11796,.F.);
#17139=ORIENTED_EDGE('',*,*,#11488,.T.);
#17140=ORIENTED_EDGE('',*,*,#11796,.T.);
#17141=ORIENTED_EDGE('',*,*,#11527,.F.);
#17142=ORIENTED_EDGE('',*,*,#11797,.F.);
#17143=ORIENTED_EDGE('',*,*,#11489,.T.);
#17144=ORIENTED_EDGE('',*,*,#11797,.T.);
#17145=ORIENTED_EDGE('',*,*,#11526,.F.);
#17146=ORIENTED_EDGE('',*,*,#11798,.F.);
#17147=ORIENTED_EDGE('',*,*,#11490,.T.);
#17148=ORIENTED_EDGE('',*,*,#11798,.T.);
#17149=ORIENTED_EDGE('',*,*,#11525,.F.);
#17150=ORIENTED_EDGE('',*,*,#11799,.F.);
#17151=ORIENTED_EDGE('',*,*,#11491,.T.);
#17152=ORIENTED_EDGE('',*,*,#11799,.T.);
#17153=ORIENTED_EDGE('',*,*,#11524,.F.);
#17154=ORIENTED_EDGE('',*,*,#11800,.F.);
#17155=ORIENTED_EDGE('',*,*,#11492,.T.);
#17156=ORIENTED_EDGE('',*,*,#11800,.T.);
#17157=ORIENTED_EDGE('',*,*,#11523,.F.);
#17158=ORIENTED_EDGE('',*,*,#11801,.F.);
#17159=ORIENTED_EDGE('',*,*,#11493,.T.);
#17160=ORIENTED_EDGE('',*,*,#11801,.T.);
#17161=ORIENTED_EDGE('',*,*,#11522,.F.);
#17162=ORIENTED_EDGE('',*,*,#11802,.F.);
#17163=ORIENTED_EDGE('',*,*,#11494,.T.);
#17164=ORIENTED_EDGE('',*,*,#11802,.T.);
#17165=ORIENTED_EDGE('',*,*,#11521,.F.);
#17166=ORIENTED_EDGE('',*,*,#11803,.F.);
#17167=ORIENTED_EDGE('',*,*,#11495,.T.);
#17168=ORIENTED_EDGE('',*,*,#11803,.T.);
#17169=ORIENTED_EDGE('',*,*,#11520,.F.);
#17170=ORIENTED_EDGE('',*,*,#11804,.F.);
#17171=ORIENTED_EDGE('',*,*,#11496,.T.);
#17172=ORIENTED_EDGE('',*,*,#11804,.T.);
#17173=ORIENTED_EDGE('',*,*,#11519,.F.);
#17174=ORIENTED_EDGE('',*,*,#11805,.F.);
#17175=ORIENTED_EDGE('',*,*,#11497,.T.);
#17176=ORIENTED_EDGE('',*,*,#11805,.T.);
#17177=ORIENTED_EDGE('',*,*,#11518,.F.);
#17178=ORIENTED_EDGE('',*,*,#11806,.F.);
#17179=ORIENTED_EDGE('',*,*,#11498,.T.);
#17180=ORIENTED_EDGE('',*,*,#11806,.T.);
#17181=ORIENTED_EDGE('',*,*,#11517,.F.);
#17182=ORIENTED_EDGE('',*,*,#11807,.F.);
#17183=ORIENTED_EDGE('',*,*,#11499,.T.);
#17184=ORIENTED_EDGE('',*,*,#11807,.T.);
#17185=ORIENTED_EDGE('',*,*,#11516,.F.);
#17186=ORIENTED_EDGE('',*,*,#11808,.F.);
#17187=ORIENTED_EDGE('',*,*,#11500,.T.);
#17188=ORIENTED_EDGE('',*,*,#11808,.T.);
#17189=ORIENTED_EDGE('',*,*,#11515,.F.);
#17190=ORIENTED_EDGE('',*,*,#11809,.F.);
#17191=ORIENTED_EDGE('',*,*,#11501,.T.);
#17192=ORIENTED_EDGE('',*,*,#11809,.T.);
#17193=ORIENTED_EDGE('',*,*,#11514,.F.);
#17194=ORIENTED_EDGE('',*,*,#11810,.F.);
#17195=ORIENTED_EDGE('',*,*,#11502,.T.);
#17196=ORIENTED_EDGE('',*,*,#11810,.T.);
#17197=ORIENTED_EDGE('',*,*,#11513,.F.);
#17198=ORIENTED_EDGE('',*,*,#11811,.F.);
#17199=ORIENTED_EDGE('',*,*,#11503,.T.);
#17200=ORIENTED_EDGE('',*,*,#11811,.T.);
#17201=ORIENTED_EDGE('',*,*,#11512,.F.);
#17202=ORIENTED_EDGE('',*,*,#11812,.F.);
#17203=ORIENTED_EDGE('',*,*,#11504,.T.);
#17204=ORIENTED_EDGE('',*,*,#11812,.T.);
#17205=ORIENTED_EDGE('',*,*,#11511,.F.);
#17206=ORIENTED_EDGE('',*,*,#11813,.F.);
#17207=ORIENTED_EDGE('',*,*,#11505,.T.);
#17208=ORIENTED_EDGE('',*,*,#11813,.T.);
#17209=ORIENTED_EDGE('',*,*,#11510,.F.);
#17210=ORIENTED_EDGE('',*,*,#11814,.F.);
#17211=ORIENTED_EDGE('',*,*,#11356,.T.);
#17212=ORIENTED_EDGE('',*,*,#11814,.T.);
#17213=ORIENTED_EDGE('',*,*,#11509,.F.);
#17214=ORIENTED_EDGE('',*,*,#11665,.F.);
#17331=CYLINDRICAL_SURFACE('',#19501,0.55);
#17332=CYLINDRICAL_SURFACE('',#19511,0.55);
#18139=ADVANCED_FACE('',(#2111),#972,.F.);
#18140=ADVANCED_FACE('',(#2112),#17331,.F.);
#18141=ADVANCED_FACE('',(#2113,#260,#261),#675,.F.);
#18142=ADVANCED_FACE('',(#2114),#973,.F.);
#18143=ADVANCED_FACE('',(#2115,#262,#263),#676,.T.);
#18144=ADVANCED_FACE('',(#2116),#974,.F.);
#18145=ADVANCED_FACE('',(#2117),#17332,.F.);
#18146=ADVANCED_FACE('',(#2118),#975,.F.);
#18147=ADVANCED_FACE('',(#2119),#677,.T.);
#18148=ADVANCED_FACE('',(#2120),#678,.T.);
#18149=ADVANCED_FACE('',(#2121),#679,.T.);
#18150=ADVANCED_FACE('',(#2122),#680,.T.);
#18151=ADVANCED_FACE('',(#2123),#681,.T.);
#18152=ADVANCED_FACE('',(#2124),#682,.T.);
#18153=ADVANCED_FACE('',(#2125),#683,.T.);
#18154=ADVANCED_FACE('',(#2126),#684,.T.);
#18155=ADVANCED_FACE('',(#2127),#685,.T.);
#18156=ADVANCED_FACE('',(#2128),#686,.T.);
#18157=ADVANCED_FACE('',(#2129),#687,.T.);
#18158=ADVANCED_FACE('',(#2130),#688,.T.);
#18159=ADVANCED_FACE('',(#2131),#689,.T.);
#18160=ADVANCED_FACE('',(#2132),#690,.T.);
#18161=ADVANCED_FACE('',(#2133),#691,.T.);
#18162=ADVANCED_FACE('',(#2134),#692,.T.);
#18163=ADVANCED_FACE('',(#2135),#693,.T.);
#18164=ADVANCED_FACE('',(#2136),#694,.T.);
#18165=ADVANCED_FACE('',(#2137),#695,.T.);
#18166=ADVANCED_FACE('',(#2138),#696,.T.);
#18167=ADVANCED_FACE('',(#2139),#697,.T.);
#18168=ADVANCED_FACE('',(#2140),#698,.T.);
#18169=ADVANCED_FACE('',(#2141),#699,.T.);
#18170=ADVANCED_FACE('',(#2142),#700,.T.);
#18171=ADVANCED_FACE('',(#2143),#701,.T.);
#18172=ADVANCED_FACE('',(#2144),#702,.T.);
#18173=ADVANCED_FACE('',(#2145),#703,.T.);
#18174=ADVANCED_FACE('',(#2146),#704,.T.);
#18175=ADVANCED_FACE('',(#2147),#705,.T.);
#18176=ADVANCED_FACE('',(#2148),#706,.T.);
#18177=ADVANCED_FACE('',(#2149),#707,.T.);
#18178=ADVANCED_FACE('',(#2150),#708,.T.);
#18179=ADVANCED_FACE('',(#2151),#709,.T.);
#18180=ADVANCED_FACE('',(#2152),#710,.T.);
#18181=ADVANCED_FACE('',(#2153),#711,.T.);
#18182=ADVANCED_FACE('',(#2154),#712,.T.);
#18183=ADVANCED_FACE('',(#2155),#713,.T.);
#18184=ADVANCED_FACE('',(#2156),#714,.T.);
#18185=ADVANCED_FACE('',(#2157),#715,.T.);
#18186=ADVANCED_FACE('',(#2158),#716,.T.);
#18187=ADVANCED_FACE('',(#2159),#717,.T.);
#18188=ADVANCED_FACE('',(#2160),#718,.T.);
#18189=ADVANCED_FACE('',(#2161),#719,.T.);
#18190=ADVANCED_FACE('',(#2162),#720,.T.);
#18191=ADVANCED_FACE('',(#2163),#721,.T.);
#18192=ADVANCED_FACE('',(#2164),#722,.T.);
#18193=ADVANCED_FACE('',(#2165),#723,.T.);
#18194=ADVANCED_FACE('',(#2166),#724,.T.);
#18195=ADVANCED_FACE('',(#2167),#725,.T.);
#18196=ADVANCED_FACE('',(#2168),#726,.T.);
#18197=ADVANCED_FACE('',(#2169),#727,.T.);
#18198=ADVANCED_FACE('',(#2170),#728,.T.);
#18199=ADVANCED_FACE('',(#2171),#729,.T.);
#18200=ADVANCED_FACE('',(#2172),#730,.T.);
#18201=ADVANCED_FACE('',(#2173),#731,.T.);
#18202=ADVANCED_FACE('',(#2174),#732,.T.);
#18203=ADVANCED_FACE('',(#2175),#733,.T.);
#18204=ADVANCED_FACE('',(#2176),#734,.T.);
#18205=ADVANCED_FACE('',(#2177),#735,.T.);
#18206=ADVANCED_FACE('',(#2178),#736,.T.);
#18207=ADVANCED_FACE('',(#2179),#737,.T.);
#18208=ADVANCED_FACE('',(#2180),#738,.T.);
#18209=ADVANCED_FACE('',(#2181),#739,.T.);
#18210=ADVANCED_FACE('',(#2182),#740,.T.);
#18211=ADVANCED_FACE('',(#2183),#741,.T.);
#18212=ADVANCED_FACE('',(#2184),#742,.T.);
#18213=ADVANCED_FACE('',(#2185),#743,.T.);
#18214=ADVANCED_FACE('',(#2186),#744,.T.);
#18215=ADVANCED_FACE('',(#2187),#745,.T.);
#18216=ADVANCED_FACE('',(#2188),#746,.T.);
#18217=ADVANCED_FACE('',(#2189),#747,.T.);
#18218=ADVANCED_FACE('',(#2190),#748,.T.);
#18219=ADVANCED_FACE('',(#2191),#749,.T.);
#18220=ADVANCED_FACE('',(#2192),#750,.T.);
#18221=ADVANCED_FACE('',(#2193),#751,.T.);
#18222=ADVANCED_FACE('',(#2194),#752,.T.);
#18223=ADVANCED_FACE('',(#2195),#753,.T.);
#18224=ADVANCED_FACE('',(#2196),#754,.T.);
#18225=ADVANCED_FACE('',(#2197),#755,.T.);
#18226=ADVANCED_FACE('',(#2198),#756,.T.);
#18227=ADVANCED_FACE('',(#2199),#757,.T.);
#18228=ADVANCED_FACE('',(#2200),#758,.T.);
#18229=ADVANCED_FACE('',(#2201),#759,.T.);
#18230=ADVANCED_FACE('',(#2202),#760,.T.);
#18231=ADVANCED_FACE('',(#2203),#761,.T.);
#18232=ADVANCED_FACE('',(#2204),#762,.T.);
#18233=ADVANCED_FACE('',(#2205),#763,.T.);
#18234=ADVANCED_FACE('',(#2206),#764,.T.);
#18235=ADVANCED_FACE('',(#2207),#765,.T.);
#18236=ADVANCED_FACE('',(#2208),#766,.T.);
#18237=ADVANCED_FACE('',(#2209),#767,.T.);
#18238=ADVANCED_FACE('',(#2210),#768,.T.);
#18239=ADVANCED_FACE('',(#2211),#769,.T.);
#18240=ADVANCED_FACE('',(#2212),#770,.T.);
#18241=ADVANCED_FACE('',(#2213),#771,.T.);
#18242=ADVANCED_FACE('',(#2214),#772,.T.);
#18243=ADVANCED_FACE('',(#2215),#773,.T.);
#18244=ADVANCED_FACE('',(#2216),#774,.T.);
#18245=ADVANCED_FACE('',(#2217),#775,.T.);
#18246=ADVANCED_FACE('',(#2218),#776,.T.);
#18247=ADVANCED_FACE('',(#2219),#777,.T.);
#18248=ADVANCED_FACE('',(#2220),#778,.T.);
#18249=ADVANCED_FACE('',(#2221),#779,.T.);
#18250=ADVANCED_FACE('',(#2222),#780,.T.);
#18251=ADVANCED_FACE('',(#2223),#781,.T.);
#18252=ADVANCED_FACE('',(#2224),#782,.T.);
#18253=ADVANCED_FACE('',(#2225),#783,.T.);
#18254=ADVANCED_FACE('',(#2226),#784,.T.);
#18255=ADVANCED_FACE('',(#2227),#785,.T.);
#18256=ADVANCED_FACE('',(#2228),#786,.T.);
#18257=ADVANCED_FACE('',(#2229),#787,.T.);
#18258=ADVANCED_FACE('',(#2230),#788,.T.);
#18259=ADVANCED_FACE('',(#2231),#789,.T.);
#18260=ADVANCED_FACE('',(#2232),#790,.T.);
#18261=ADVANCED_FACE('',(#2233),#791,.T.);
#18262=ADVANCED_FACE('',(#2234),#792,.T.);
#18263=ADVANCED_FACE('',(#2235),#793,.T.);
#18264=ADVANCED_FACE('',(#2236),#794,.T.);
#18265=ADVANCED_FACE('',(#2237),#795,.T.);
#18266=ADVANCED_FACE('',(#2238),#796,.T.);
#18267=ADVANCED_FACE('',(#2239),#797,.T.);
#18268=ADVANCED_FACE('',(#2240),#798,.T.);
#18269=ADVANCED_FACE('',(#2241),#799,.T.);
#18270=ADVANCED_FACE('',(#2242),#800,.T.);
#18271=ADVANCED_FACE('',(#2243),#801,.T.);
#18272=ADVANCED_FACE('',(#2244),#802,.T.);
#18273=ADVANCED_FACE('',(#2245),#803,.T.);
#18274=ADVANCED_FACE('',(#2246),#804,.T.);
#18275=ADVANCED_FACE('',(#2247),#805,.T.);
#18276=ADVANCED_FACE('',(#2248),#806,.T.);
#18277=ADVANCED_FACE('',(#2249),#807,.T.);
#18278=ADVANCED_FACE('',(#2250),#808,.T.);
#18279=ADVANCED_FACE('',(#2251),#809,.T.);
#18280=ADVANCED_FACE('',(#2252),#810,.T.);
#18281=ADVANCED_FACE('',(#2253),#811,.T.);
#18282=ADVANCED_FACE('',(#2254),#812,.T.);
#18283=ADVANCED_FACE('',(#2255),#813,.T.);
#18284=ADVANCED_FACE('',(#2256),#814,.T.);
#18285=ADVANCED_FACE('',(#2257),#815,.T.);
#18286=ADVANCED_FACE('',(#2258),#816,.T.);
#18287=ADVANCED_FACE('',(#2259),#817,.T.);
#18288=ADVANCED_FACE('',(#2260),#818,.T.);
#18289=ADVANCED_FACE('',(#2261),#819,.T.);
#18290=ADVANCED_FACE('',(#2262),#820,.T.);
#18291=ADVANCED_FACE('',(#2263),#821,.T.);
#18292=ADVANCED_FACE('',(#2264),#822,.T.);
#18293=ADVANCED_FACE('',(#2265),#823,.T.);
#18294=ADVANCED_FACE('',(#2266),#824,.T.);
#18295=ADVANCED_FACE('',(#2267),#825,.T.);
#18296=ADVANCED_FACE('',(#2268),#826,.T.);
#18306=CLOSED_SHELL('',(#18139,#18140,#18141,#18142,#18143,#18144,#18145,
#18146,#18147,#18148,#18149,#18150,#18151,#18152,#18153,#18154,#18155,#18156,
#18157,#18158,#18159,#18160,#18161,#18162,#18163,#18164,#18165,#18166,#18167,
#18168,#18169,#18170,#18171,#18172,#18173,#18174,#18175,#18176,#18177,#18178,
#18179,#18180,#18181,#18182,#18183,#18184,#18185,#18186,#18187,#18188,#18189,
#18190,#18191,#18192,#18193,#18194,#18195,#18196,#18197,#18198,#18199,#18200,
#18201,#18202,#18203,#18204,#18205,#18206,#18207,#18208,#18209,#18210,#18211,
#18212,#18213,#18214,#18215,#18216,#18217,#18218,#18219,#18220,#18221,#18222,
#18223,#18224,#18225,#18226,#18227,#18228,#18229,#18230,#18231,#18232,#18233,
#18234,#18235,#18236,#18237,#18238,#18239,#18240,#18241,#18242,#18243,#18244,
#18245,#18246,#18247,#18248,#18249,#18250,#18251,#18252,#18253,#18254,#18255,
#18256,#18257,#18258,#18259,#18260,#18261,#18262,#18263,#18264,#18265,#18266,
#18267,#18268,#18269,#18270,#18271,#18272,#18273,#18274,#18275,#18276,#18277,
#18278,#18279,#18280,#18281,#18282,#18283,#18284,#18285,#18286,#18287,#18288,
#18289,#18290,#18291,#18292,#18293,#18294,#18295,#18296));
#19497=AXIS2_PLACEMENT_3D('',#59397,#22792,#22793);
#19498=AXIS2_PLACEMENT_3D('',#59398,#22794,#22795);
#19499=AXIS2_PLACEMENT_3D('',#59400,#22796,#22797);
#19500=AXIS2_PLACEMENT_3D('',#59403,#22799,#22800);
#19501=AXIS2_PLACEMENT_3D('',#59404,#22801,#22802);
#19502=AXIS2_PLACEMENT_3D('',#59407,#22804,#22805);
#19503=AXIS2_PLACEMENT_3D('',#59408,#22806,#22807);
#19504=AXIS2_PLACEMENT_3D('',#59710,#22958,#22959);
#19505=AXIS2_PLACEMENT_3D('',#59711,#22960,#22961);
#19506=AXIS2_PLACEMENT_3D('',#59713,#22962,#22963);
#19507=AXIS2_PLACEMENT_3D('',#59715,#22965,#22966);
#19508=AXIS2_PLACEMENT_3D('',#60017,#23117,#23118);
#19509=AXIS2_PLACEMENT_3D('',#60018,#23119,#23120);
#19510=AXIS2_PLACEMENT_3D('',#60021,#23122,#23123);
#19511=AXIS2_PLACEMENT_3D('',#60022,#23124,#23125);
#19512=AXIS2_PLACEMENT_3D('',#60025,#23127,#23128);
#19513=AXIS2_PLACEMENT_3D('',#60026,#23129,#23130);
#19514=AXIS2_PLACEMENT_3D('',#60028,#23132,#23133);
#19515=AXIS2_PLACEMENT_3D('',#60031,#23136,#23137);
#19516=AXIS2_PLACEMENT_3D('',#60033,#23139,#23140);
#19517=AXIS2_PLACEMENT_3D('',#60035,#23142,#23143);
#19518=AXIS2_PLACEMENT_3D('',#60037,#23145,#23146);
#19519=AXIS2_PLACEMENT_3D('',#60039,#23148,#23149);
#19520=AXIS2_PLACEMENT_3D('',#60041,#23151,#23152);
#19521=AXIS2_PLACEMENT_3D('',#60043,#23154,#23155);
#19522=AXIS2_PLACEMENT_3D('',#60045,#23157,#23158);
#19523=AXIS2_PLACEMENT_3D('',#60047,#23160,#23161);
#19524=AXIS2_PLACEMENT_3D('',#60049,#23163,#23164);
#19525=AXIS2_PLACEMENT_3D('',#60051,#23166,#23167);
#19526=AXIS2_PLACEMENT_3D('',#60053,#23169,#23170);
#19527=AXIS2_PLACEMENT_3D('',#60055,#23172,#23173);
#19528=AXIS2_PLACEMENT_3D('',#60057,#23175,#23176);
#19529=AXIS2_PLACEMENT_3D('',#60059,#23178,#23179);
#19530=AXIS2_PLACEMENT_3D('',#60061,#23181,#23182);
#19531=AXIS2_PLACEMENT_3D('',#60063,#23184,#23185);
#19532=AXIS2_PLACEMENT_3D('',#60065,#23187,#23188);
#19533=AXIS2_PLACEMENT_3D('',#60067,#23190,#23191);
#19534=AXIS2_PLACEMENT_3D('',#60069,#23193,#23194);
#19535=AXIS2_PLACEMENT_3D('',#60071,#23196,#23197);
#19536=AXIS2_PLACEMENT_3D('',#60073,#23199,#23200);
#19537=AXIS2_PLACEMENT_3D('',#60075,#23202,#23203);
#19538=AXIS2_PLACEMENT_3D('',#60077,#23205,#23206);
#19539=AXIS2_PLACEMENT_3D('',#60079,#23208,#23209);
#19540=AXIS2_PLACEMENT_3D('',#60081,#23211,#23212);
#19541=AXIS2_PLACEMENT_3D('',#60083,#23214,#23215);
#19542=AXIS2_PLACEMENT_3D('',#60085,#23217,#23218);
#19543=AXIS2_PLACEMENT_3D('',#60087,#23220,#23221);
#19544=AXIS2_PLACEMENT_3D('',#60089,#23223,#23224);
#19545=AXIS2_PLACEMENT_3D('',#60091,#23226,#23227);
#19546=AXIS2_PLACEMENT_3D('',#60093,#23229,#23230);
#19547=AXIS2_PLACEMENT_3D('',#60095,#23232,#23233);
#19548=AXIS2_PLACEMENT_3D('',#60097,#23235,#23236);
#19549=AXIS2_PLACEMENT_3D('',#60099,#23238,#23239);
#19550=AXIS2_PLACEMENT_3D('',#60101,#23241,#23242);
#19551=AXIS2_PLACEMENT_3D('',#60103,#23244,#23245);
#19552=AXIS2_PLACEMENT_3D('',#60105,#23247,#23248);
#19553=AXIS2_PLACEMENT_3D('',#60107,#23250,#23251);
#19554=AXIS2_PLACEMENT_3D('',#60109,#23253,#23254);
#19555=AXIS2_PLACEMENT_3D('',#60111,#23256,#23257);
#19556=AXIS2_PLACEMENT_3D('',#60113,#23259,#23260);
#19557=AXIS2_PLACEMENT_3D('',#60115,#23262,#23263);
#19558=AXIS2_PLACEMENT_3D('',#60117,#23265,#23266);
#19559=AXIS2_PLACEMENT_3D('',#60119,#23268,#23269);
#19560=AXIS2_PLACEMENT_3D('',#60121,#23271,#23272);
#19561=AXIS2_PLACEMENT_3D('',#60123,#23274,#23275);
#19562=AXIS2_PLACEMENT_3D('',#60125,#23277,#23278);
#19563=AXIS2_PLACEMENT_3D('',#60127,#23280,#23281);
#19564=AXIS2_PLACEMENT_3D('',#60129,#23283,#23284);
#19565=AXIS2_PLACEMENT_3D('',#60131,#23286,#23287);
#19566=AXIS2_PLACEMENT_3D('',#60133,#23289,#23290);
#19567=AXIS2_PLACEMENT_3D('',#60135,#23292,#23293);
#19568=AXIS2_PLACEMENT_3D('',#60137,#23295,#23296);
#19569=AXIS2_PLACEMENT_3D('',#60139,#23298,#23299);
#19570=AXIS2_PLACEMENT_3D('',#60141,#23301,#23302);
#19571=AXIS2_PLACEMENT_3D('',#60143,#23304,#23305);
#19572=AXIS2_PLACEMENT_3D('',#60145,#23307,#23308);
#19573=AXIS2_PLACEMENT_3D('',#60147,#23310,#23311);
#19574=AXIS2_PLACEMENT_3D('',#60149,#23313,#23314);
#19575=AXIS2_PLACEMENT_3D('',#60151,#23316,#23317);
#19576=AXIS2_PLACEMENT_3D('',#60153,#23319,#23320);
#19577=AXIS2_PLACEMENT_3D('',#60155,#23322,#23323);
#19578=AXIS2_PLACEMENT_3D('',#60157,#23325,#23326);
#19579=AXIS2_PLACEMENT_3D('',#60159,#23328,#23329);
#19580=AXIS2_PLACEMENT_3D('',#60161,#23331,#23332);
#19581=AXIS2_PLACEMENT_3D('',#60163,#23334,#23335);
#19582=AXIS2_PLACEMENT_3D('',#60165,#23337,#23338);
#19583=AXIS2_PLACEMENT_3D('',#60167,#23340,#23341);
#19584=AXIS2_PLACEMENT_3D('',#60169,#23343,#23344);
#19585=AXIS2_PLACEMENT_3D('',#60171,#23346,#23347);
#19586=AXIS2_PLACEMENT_3D('',#60173,#23349,#23350);
#19587=AXIS2_PLACEMENT_3D('',#60175,#23352,#23353);
#19588=AXIS2_PLACEMENT_3D('',#60177,#23355,#23356);
#19589=AXIS2_PLACEMENT_3D('',#60179,#23358,#23359);
#19590=AXIS2_PLACEMENT_3D('',#60181,#23361,#23362);
#19591=AXIS2_PLACEMENT_3D('',#60183,#23364,#23365);
#19592=AXIS2_PLACEMENT_3D('',#60185,#23367,#23368);
#19593=AXIS2_PLACEMENT_3D('',#60187,#23370,#23371);
#19594=AXIS2_PLACEMENT_3D('',#60189,#23373,#23374);
#19595=AXIS2_PLACEMENT_3D('',#60191,#23376,#23377);
#19596=AXIS2_PLACEMENT_3D('',#60193,#23379,#23380);
#19597=AXIS2_PLACEMENT_3D('',#60195,#23382,#23383);
#19598=AXIS2_PLACEMENT_3D('',#60197,#23385,#23386);
#19599=AXIS2_PLACEMENT_3D('',#60199,#23388,#23389);
#19600=AXIS2_PLACEMENT_3D('',#60201,#23391,#23392);
#19601=AXIS2_PLACEMENT_3D('',#60203,#23394,#23395);
#19602=AXIS2_PLACEMENT_3D('',#60205,#23397,#23398);
#19603=AXIS2_PLACEMENT_3D('',#60207,#23400,#23401);
#19604=AXIS2_PLACEMENT_3D('',#60209,#23403,#23404);
#19605=AXIS2_PLACEMENT_3D('',#60211,#23406,#23407);
#19606=AXIS2_PLACEMENT_3D('',#60213,#23409,#23410);
#19607=AXIS2_PLACEMENT_3D('',#60215,#23412,#23413);
#19608=AXIS2_PLACEMENT_3D('',#60217,#23415,#23416);
#19609=AXIS2_PLACEMENT_3D('',#60219,#23418,#23419);
#19610=AXIS2_PLACEMENT_3D('',#60221,#23421,#23422);
#19611=AXIS2_PLACEMENT_3D('',#60223,#23424,#23425);
#19612=AXIS2_PLACEMENT_3D('',#60225,#23427,#23428);
#19613=AXIS2_PLACEMENT_3D('',#60227,#23430,#23431);
#19614=AXIS2_PLACEMENT_3D('',#60229,#23433,#23434);
#19615=AXIS2_PLACEMENT_3D('',#60231,#23436,#23437);
#19616=AXIS2_PLACEMENT_3D('',#60233,#23439,#23440);
#19617=AXIS2_PLACEMENT_3D('',#60235,#23442,#23443);
#19618=AXIS2_PLACEMENT_3D('',#60237,#23445,#23446);
#19619=AXIS2_PLACEMENT_3D('',#60239,#23448,#23449);
#19620=AXIS2_PLACEMENT_3D('',#60241,#23451,#23452);
#19621=AXIS2_PLACEMENT_3D('',#60243,#23454,#23455);
#19622=AXIS2_PLACEMENT_3D('',#60245,#23457,#23458);
#19623=AXIS2_PLACEMENT_3D('',#60247,#23460,#23461);
#19624=AXIS2_PLACEMENT_3D('',#60249,#23463,#23464);
#19625=AXIS2_PLACEMENT_3D('',#60251,#23466,#23467);
#19626=AXIS2_PLACEMENT_3D('',#60253,#23469,#23470);
#19627=AXIS2_PLACEMENT_3D('',#60255,#23472,#23473);
#19628=AXIS2_PLACEMENT_3D('',#60257,#23475,#23476);
#19629=AXIS2_PLACEMENT_3D('',#60259,#23478,#23479);
#19630=AXIS2_PLACEMENT_3D('',#60261,#23481,#23482);
#19631=AXIS2_PLACEMENT_3D('',#60263,#23484,#23485);
#19632=AXIS2_PLACEMENT_3D('',#60265,#23487,#23488);
#19633=AXIS2_PLACEMENT_3D('',#60267,#23490,#23491);
#19634=AXIS2_PLACEMENT_3D('',#60269,#23493,#23494);
#19635=AXIS2_PLACEMENT_3D('',#60271,#23496,#23497);
#19636=AXIS2_PLACEMENT_3D('',#60273,#23499,#23500);
#19637=AXIS2_PLACEMENT_3D('',#60275,#23502,#23503);
#19638=AXIS2_PLACEMENT_3D('',#60277,#23505,#23506);
#19639=AXIS2_PLACEMENT_3D('',#60279,#23508,#23509);
#19640=AXIS2_PLACEMENT_3D('',#60281,#23511,#23512);
#19641=AXIS2_PLACEMENT_3D('',#60283,#23514,#23515);
#19642=AXIS2_PLACEMENT_3D('',#60285,#23517,#23518);
#19643=AXIS2_PLACEMENT_3D('',#60287,#23520,#23521);
#19644=AXIS2_PLACEMENT_3D('',#60289,#23523,#23524);
#19645=AXIS2_PLACEMENT_3D('',#60291,#23526,#23527);
#19646=AXIS2_PLACEMENT_3D('',#60293,#23529,#23530);
#19647=AXIS2_PLACEMENT_3D('',#60295,#23532,#23533);
#19648=AXIS2_PLACEMENT_3D('',#60297,#23535,#23536);
#19649=AXIS2_PLACEMENT_3D('',#60299,#23538,#23539);
#19650=AXIS2_PLACEMENT_3D('',#60301,#23541,#23542);
#19651=AXIS2_PLACEMENT_3D('',#60303,#23544,#23545);
#19652=AXIS2_PLACEMENT_3D('',#60305,#23547,#23548);
#19653=AXIS2_PLACEMENT_3D('',#60307,#23550,#23551);
#19654=AXIS2_PLACEMENT_3D('',#60309,#23553,#23554);
#19655=AXIS2_PLACEMENT_3D('',#60311,#23556,#23557);
#19656=AXIS2_PLACEMENT_3D('',#60313,#23559,#23560);
#19657=AXIS2_PLACEMENT_3D('',#60315,#23562,#23563);
#19658=AXIS2_PLACEMENT_3D('',#60317,#23565,#23566);
#19659=AXIS2_PLACEMENT_3D('',#60319,#23568,#23569);
#19660=AXIS2_PLACEMENT_3D('',#60321,#23571,#23572);
#19661=AXIS2_PLACEMENT_3D('',#60323,#23574,#23575);
#19662=AXIS2_PLACEMENT_3D('',#60325,#23577,#23578);
#19663=AXIS2_PLACEMENT_3D('',#60327,#23580,#23581);
#22792=DIRECTION('axis',(0.,0.,1.));
#22793=DIRECTION('refdir',(1.,0.,0.));
#22794=DIRECTION('center_axis',(-1.,0.,0.));
#22795=DIRECTION('ref_axis',(0.,0.,-1.));
#22796=DIRECTION('center_axis',(-1.,0.,0.));
#22797=DIRECTION('ref_axis',(0.,0.,-1.));
#22798=DIRECTION('',(0.707106781186547,-8.65956056235494E-17,-0.707106781186548));
#22799=DIRECTION('center_axis',(1.,0.,0.));
#22800=DIRECTION('ref_axis',(0.,0.,-1.));
#22801=DIRECTION('center_axis',(1.,0.,0.));
#22802=DIRECTION('ref_axis',(0.,0.,-1.));
#22803=DIRECTION('',(1.,0.,0.));
#22804=DIRECTION('center_axis',(-1.,0.,0.));
#22805=DIRECTION('ref_axis',(0.,0.,-1.));
#22806=DIRECTION('center_axis',(1.,0.,0.));
#22807=DIRECTION('ref_axis',(0.,0.,-1.));
#22808=DIRECTION('',(0.,-0.275637355816999,0.961261695938319));
#22809=DIRECTION('',(0.,0.923879532511287,0.382683432365089));
#22810=DIRECTION('',(0.,0.48480962024634,-0.874619707139394));
#22811=DIRECTION('',(0.,0.856292125836473,0.516491815259888));
#22812=DIRECTION('',(0.,0.816221627432192,0.577738915871126));
#22813=DIRECTION('',(0.,0.771778750427187,0.635891154513923));
#22814=DIRECTION('',(0.,0.723201568743836,0.690637018242183));
#22815=DIRECTION('',(0.,0.670750303163526,0.741683241556689));
#22816=DIRECTION('',(0.,0.614705927362395,0.788756377385019));
#22817=DIRECTION('',(0.,0.555368662776888,0.831604261897095));
#22818=DIRECTION('',(0.,0.493056370361897,0.869997365309546));
#22819=DIRECTION('',(0.,0.428102847856614,0.903730021442829));
#22820=DIRECTION('',(0.,0.360856041679385,0.932621529444547));
#22821=DIRECTION('',(0.,0.291676183030194,0.956517121777199));
#22822=DIRECTION('',(0.,0.22093385818535,0.975288793285012));
#22823=DIRECTION('',(0.,0.14900802332161,0.98883598689863));
#22824=DIRECTION('',(0.,0.0762839745039533,0.997086132304467));
#22825=DIRECTION('',(0.,0.00315128371150461,0.999995034693158));
#22826=DIRECTION('',(0.,-0.069998288041949,0.997547111504613));
#22827=DIRECTION('',(0.,-0.142772889313813,0.98975547590149));
#22828=DIRECTION('',(0.,-0.214782677322933,0.976661866523923));
#22829=DIRECTION('',(0.,-0.285641906279744,0.958336423901791));
#22830=DIRECTION('',(0.,-0.354970993769443,0.934877314722276));
#22831=DIRECTION('',(0.,-0.422398554118871,0.906410205965427));
#22832=DIRECTION('',(0.,-0.487563387854682,0.873087591724716));
#22833=DIRECTION('',(0.,-0.550116416595493,0.835087976318743));
#22834=DIRECTION('',(0.,-0.609722553013204,0.792614918069967));
#22835=DIRECTION('',(0.,-0.666062495846264,0.745895938872873));
#22836=DIRECTION('',(0.,-0.718834440349327,0.695181305392823));
#22837=DIRECTION('',(0.,-0.767755695016677,0.640742688424503));
#22838=DIRECTION('',(0.,-0.812564195918804,0.582871707591668));
#22839=DIRECTION('',(0.,-0.853019910540169,0.521878369183895));
#22840=DIRECTION('',(0.,-0.888906123597886,0.458089405498731));
#22841=DIRECTION('',(0.,-0.920030597953456,0.39184652458508));
#22842=DIRECTION('',(0.,-0.946226604398715,0.323504579763685));
#22843=DIRECTION('',(0.,-0.967353814799542,0.253429668730349));
#22844=DIRECTION('',(0.,-0.983299053812935,0.181997172424701));
#22845=DIRECTION('',(0.,-0.993976905150596,0.109589744169988));
#22846=DIRECTION('',(0.,-0.999330169141354,0.0365952598557893));
#22847=DIRECTION('',(0.,-0.999330169141354,-0.0365952598557893));
#22848=DIRECTION('',(0.,-0.993976905150596,-0.109589744169987));
#22849=DIRECTION('',(0.,-0.983299053812935,-0.181997172424701));
#22850=DIRECTION('',(0.,-0.967353814799542,-0.253429668730349));
#22851=DIRECTION('',(0.,-0.946226604398715,-0.323504579763685));
#22852=DIRECTION('',(0.,-0.920030597953456,-0.39184652458508));
#22853=DIRECTION('',(0.,-0.888906123597886,-0.458089405498731));
#22854=DIRECTION('',(0.,-0.85301991054017,-0.521878369183893));
#22855=DIRECTION('',(0.,-0.812564195918805,-0.582871707591668));
#22856=DIRECTION('',(0.,-0.767755695016675,-0.640742688424505));
#22857=DIRECTION('',(0.,-0.71883444034933,-0.69518130539282));
#22858=DIRECTION('',(0.,-0.666062495846262,-0.745895938872875));
#22859=DIRECTION('',(0.,-0.609722553013205,-0.792614918069966));
#22860=DIRECTION('',(0.,-0.550116416595494,-0.835087976318742));
#22861=DIRECTION('',(0.,-0.48756338785468,-0.873087591724717));
#22862=DIRECTION('',(0.,-0.422398554118875,-0.906410205965425));
#22863=DIRECTION('',(0.,-0.354970993769442,-0.934877314722277));
#22864=DIRECTION('',(0.,-0.285641906279744,-0.958336423901791));
#22865=DIRECTION('',(0.,-0.214782677322933,-0.976661866523923));
#22866=DIRECTION('',(0.,-0.142772889313813,-0.98975547590149));
#22867=DIRECTION('',(0.,-0.0699982880419509,-0.997547111504613));
#22868=DIRECTION('',(0.,0.00315128371150461,-0.999995034693158));
#22869=DIRECTION('',(0.,0.0762839745039523,-0.997086132304467));
#22870=DIRECTION('',(0.,0.14900802332161,-0.98883598689863));
#22871=DIRECTION('',(0.,0.220933858185349,-0.975288793285013));
#22872=DIRECTION('',(0.,0.291676183030194,-0.956517121777199));
#22873=DIRECTION('',(0.,0.360856041679387,-0.932621529444546));
#22874=DIRECTION('',(0.,0.428102847856613,-0.90373002144283));
#22875=DIRECTION('',(0.,0.493056370361895,-0.869997365309547));
#22876=DIRECTION('',(0.,0.555368662776888,-0.831604261897095));
#22877=DIRECTION('',(0.,0.614705927362394,-0.788756377385019));
#22878=DIRECTION('',(0.,0.670750303163526,-0.741683241556689));
#22879=DIRECTION('',(0.,0.723201568743836,-0.690637018242184));
#22880=DIRECTION('',(0.,0.771778750427186,-0.635891154513924));
#22881=DIRECTION('',(0.,0.816221627432192,-0.577738915871126));
#22882=DIRECTION('',(0.,0.856292125836472,-0.516491815259888));
#22883=DIRECTION('',(0.,0.484809620246337,0.874619707139396));
#22884=DIRECTION('',(0.,0.923879532511286,-0.382683432365091));
#22885=DIRECTION('',(0.,-0.275637355817,-0.961261695938319));
#22886=DIRECTION('',(0.,-0.94954718849933,0.313624196791349));
#22887=DIRECTION('',(0.,-0.921637548163022,0.388051839083456));
#22888=DIRECTION('',(0.,-0.887904612902449,0.460027606113537));
#22889=DIRECTION('',(0.,-0.848561521636558,0.529096724614553));
#22890=DIRECTION('',(0.,-0.803856860617217,0.594822786751342));
#22891=DIRECTION('',(0.,-0.754073092756362,0.656790507529498));
#22892=DIRECTION('',(0.,-0.699524772906136,0.714608348741196));
#22893=DIRECTION('',(0.,-0.640556560368615,0.767910992868789));
#22894=DIRECTION('',(0.,-0.577541041192885,0.816361651315052));
#22895=DIRECTION('',(0.,-0.51087637401918,0.85965419237564));
#22896=DIRECTION('',(0.,-0.44098377434459,0.897515075508373));
#22897=DIRECTION('',(0.,-0.368304853105793,0.929705079677808));
#22898=DIRECTION('',(0.,-0.293298826394844,0.95602081485468));
#22899=DIRECTION('',(0.,-0.2164396139381,0.976296007119934));
#22900=DIRECTION('',(0.,-0.138212844671456,0.990402549253496));
#22901=DIRECTION('',(0.,-0.0591127883317614,0.998251310169761));
#22902=DIRECTION('',(0.,0.0203607675478923,0.999792698085389));
#22903=DIRECTION('',(0.,0.0997056755067372,0.995016973861122));
#22904=DIRECTION('',(0.,0.178420600935832,0.983954312537781));
#22905=DIRECTION('',(0.,0.256008189721705,0.966674612677614));
#22906=DIRECTION('',(0.,0.331978210739482,0.943287054715696));
#22907=DIRECTION('',(0.,0.405850653339991,0.913939411111865));
#22908=DIRECTION('',(0.,0.47715876025961,0.878817112661964));
#22909=DIRECTION('',(0.,0.545451976789583,0.83814207686784));
#22910=DIRECTION('',(0.,0.610298797570814,0.792171305768909));
#22911=DIRECTION('',(0.,0.671289493026783,0.741195262094844));
#22912=DIRECTION('',(0.,0.728038698207918,0.685536033999469));
#22913=DIRECTION('',(0.,0.780187847689935,0.62554529997191));
#22914=DIRECTION('',(0.,0.827407441141511,0.561602106783492));
#22915=DIRECTION('',(0.,0.869399125246396,0.494110474510307));
#22916=DIRECTION('',(0.,0.905897578825568,0.423496843763887));
#22917=DIRECTION('',(0.,0.936672189248398,0.350207381259467));
#22918=DIRECTION('',(0.,0.96152850954055,0.274705160746442));
#22919=DIRECTION('',(0.,0.980309486982024,0.197467237112997));
#22920=DIRECTION('',(0.,0.992896455432508,0.118981632152029));
#22921=DIRECTION('',(0.,0.999209885114126,0.0397442510335229));
#22922=DIRECTION('',(0.,0.999209885114126,-0.0397442510335258));
#22923=DIRECTION('',(0.,0.992896455432509,-0.118981632152026));
#22924=DIRECTION('',(0.,0.980309486982024,-0.197467237112996));
#22925=DIRECTION('',(0.,0.961528509540549,-0.274705160746445));
#22926=DIRECTION('',(0.,0.936672189248397,-0.350207381259469));
#22927=DIRECTION('',(0.,0.90589757882557,-0.423496843763883));
#22928=DIRECTION('',(0.,0.869399125246396,-0.494110474510309));
#22929=DIRECTION('',(0.,0.827407441141511,-0.561602106783492));
#22930=DIRECTION('',(0.,0.780187847689935,-0.62554529997191));
#22931=DIRECTION('',(0.,0.728038698207917,-0.685536033999469));
#22932=DIRECTION('',(0.,0.671289493026782,-0.741195262094845));
#22933=DIRECTION('',(0.,0.610298797570813,-0.79217130576891));
#22934=DIRECTION('',(0.,0.545451976789582,-0.83814207686784));
#22935=DIRECTION('',(0.,0.477158760259606,-0.878817112661967));
#22936=DIRECTION('',(0.,0.405850653339993,-0.913939411111864));
#22937=DIRECTION('',(0.,0.33197821073948,-0.943287054715696));
#22938=DIRECTION('',(0.,0.256008189721705,-0.966674612677614));
#22939=DIRECTION('',(0.,0.178420600935832,-0.983954312537781));
#22940=DIRECTION('',(0.,0.0997056755067357,-0.995016973861122));
#22941=DIRECTION('',(0.,0.0203607675478923,-0.999792698085389));
#22942=DIRECTION('',(0.,-0.0591127883317644,-0.998251310169761));
#22943=DIRECTION('',(0.,-0.138212844671453,-0.990402549253497));
#22944=DIRECTION('',(0.,-0.216439613938106,-0.976296007119933));
#22945=DIRECTION('',(0.,-0.293298826394842,-0.956020814854681));
#22946=DIRECTION('',(0.,-0.368304853105795,-0.929705079677808));
#22947=DIRECTION('',(0.,-0.44098377434459,-0.897515075508373));
#22948=DIRECTION('',(0.,-0.510876374019181,-0.85965419237564));
#22949=DIRECTION('',(0.,-0.577541041192886,-0.816361651315051));
#22950=DIRECTION('',(0.,-0.640556560368615,-0.767910992868789));
#22951=DIRECTION('',(0.,-0.699524772906137,-0.714608348741195));
#22952=DIRECTION('',(0.,-0.754073092756361,-0.656790507529498));
#22953=DIRECTION('',(0.,-0.803856860617218,-0.59482278675134));
#22954=DIRECTION('',(0.,-0.848561521636558,-0.529096724614554));
#22955=DIRECTION('',(0.,-0.88790461290245,-0.460027606113536));
#22956=DIRECTION('',(0.,-0.921637548163023,-0.388051839083454));
#22957=DIRECTION('',(0.,-0.94954718849933,-0.313624196791348));
#22958=DIRECTION('center_axis',(-1.,0.,0.));
#22959=DIRECTION('ref_axis',(0.,0.,-1.));
#22960=DIRECTION('center_axis',(1.,0.,0.));
#22961=DIRECTION('ref_axis',(0.,0.,-1.));
#22962=DIRECTION('center_axis',(1.,0.,0.));
#22963=DIRECTION('ref_axis',(0.,0.,-1.));
#22964=DIRECTION('',(-0.707106781186547,8.65956056235494E-17,-0.707106781186548));
#22965=DIRECTION('center_axis',(1.,0.,0.));
#22966=DIRECTION('ref_axis',(0.,0.,-1.));
#22967=DIRECTION('',(0.,-0.275637355816999,0.961261695938319));
#22968=DIRECTION('',(0.,-0.94954718849933,-0.313624196791348));
#22969=DIRECTION('',(0.,-0.921637548163023,-0.388051839083454));
#22970=DIRECTION('',(0.,-0.88790461290245,-0.460027606113536));
#22971=DIRECTION('',(0.,-0.848561521636558,-0.529096724614554));
#22972=DIRECTION('',(0.,-0.803856860617218,-0.59482278675134));
#22973=DIRECTION('',(0.,-0.754073092756361,-0.656790507529498));
#22974=DIRECTION('',(0.,-0.699524772906137,-0.714608348741195));
#22975=DIRECTION('',(0.,-0.640556560368615,-0.767910992868789));
#22976=DIRECTION('',(0.,-0.577541041192886,-0.816361651315051));
#22977=DIRECTION('',(0.,-0.510876374019181,-0.85965419237564));
#22978=DIRECTION('',(0.,-0.44098377434459,-0.897515075508373));
#22979=DIRECTION('',(0.,-0.368304853105795,-0.929705079677808));
#22980=DIRECTION('',(0.,-0.293298826394842,-0.956020814854681));
#22981=DIRECTION('',(0.,-0.216439613938106,-0.976296007119933));
#22982=DIRECTION('',(0.,-0.138212844671453,-0.990402549253497));
#22983=DIRECTION('',(0.,-0.0591127883317644,-0.998251310169761));
#22984=DIRECTION('',(0.,0.0203607675478923,-0.999792698085389));
#22985=DIRECTION('',(0.,0.0997056755067357,-0.995016973861122));
#22986=DIRECTION('',(0.,0.178420600935832,-0.983954312537781));
#22987=DIRECTION('',(0.,0.256008189721705,-0.966674612677614));
#22988=DIRECTION('',(0.,0.33197821073948,-0.943287054715696));
#22989=DIRECTION('',(0.,0.405850653339993,-0.913939411111864));
#22990=DIRECTION('',(0.,0.477158760259606,-0.878817112661967));
#22991=DIRECTION('',(0.,0.545451976789582,-0.83814207686784));
#22992=DIRECTION('',(0.,0.610298797570813,-0.79217130576891));
#22993=DIRECTION('',(0.,0.671289493026782,-0.741195262094845));
#22994=DIRECTION('',(0.,0.728038698207917,-0.685536033999469));
#22995=DIRECTION('',(0.,0.780187847689935,-0.62554529997191));
#22996=DIRECTION('',(0.,0.827407441141511,-0.561602106783492));
#22997=DIRECTION('',(0.,0.869399125246396,-0.494110474510309));
#22998=DIRECTION('',(0.,0.90589757882557,-0.423496843763883));
#22999=DIRECTION('',(0.,0.936672189248397,-0.350207381259469));
#23000=DIRECTION('',(0.,0.961528509540549,-0.274705160746445));
#23001=DIRECTION('',(0.,0.980309486982024,-0.197467237112996));
#23002=DIRECTION('',(0.,0.992896455432509,-0.118981632152026));
#23003=DIRECTION('',(0.,0.999209885114126,-0.0397442510335258));
#23004=DIRECTION('',(0.,0.999209885114126,0.0397442510335229));
#23005=DIRECTION('',(0.,0.992896455432508,0.118981632152029));
#23006=DIRECTION('',(0.,0.980309486982024,0.197467237112997));
#23007=DIRECTION('',(0.,0.96152850954055,0.274705160746442));
#23008=DIRECTION('',(0.,0.936672189248398,0.350207381259467));
#23009=DIRECTION('',(0.,0.905897578825568,0.423496843763887));
#23010=DIRECTION('',(0.,0.869399125246396,0.494110474510307));
#23011=DIRECTION('',(0.,0.827407441141511,0.561602106783492));
#23012=DIRECTION('',(0.,0.780187847689935,0.62554529997191));
#23013=DIRECTION('',(0.,0.728038698207918,0.685536033999469));
#23014=DIRECTION('',(0.,0.671289493026783,0.741195262094844));
#23015=DIRECTION('',(0.,0.610298797570814,0.792171305768909));
#23016=DIRECTION('',(0.,0.545451976789583,0.83814207686784));
#23017=DIRECTION('',(0.,0.47715876025961,0.878817112661964));
#23018=DIRECTION('',(0.,0.405850653339991,0.913939411111865));
#23019=DIRECTION('',(0.,0.331978210739482,0.943287054715696));
#23020=DIRECTION('',(0.,0.256008189721705,0.966674612677614));
#23021=DIRECTION('',(0.,0.178420600935832,0.983954312537781));
#23022=DIRECTION('',(0.,0.0997056755067372,0.995016973861122));
#23023=DIRECTION('',(0.,0.0203607675478923,0.999792698085389));
#23024=DIRECTION('',(0.,-0.0591127883317614,0.998251310169761));
#23025=DIRECTION('',(0.,-0.138212844671456,0.990402549253496));
#23026=DIRECTION('',(0.,-0.2164396139381,0.976296007119934));
#23027=DIRECTION('',(0.,-0.293298826394844,0.95602081485468));
#23028=DIRECTION('',(0.,-0.368304853105793,0.929705079677808));
#23029=DIRECTION('',(0.,-0.44098377434459,0.897515075508373));
#23030=DIRECTION('',(0.,-0.51087637401918,0.85965419237564));
#23031=DIRECTION('',(0.,-0.577541041192885,0.816361651315052));
#23032=DIRECTION('',(0.,-0.640556560368615,0.767910992868789));
#23033=DIRECTION('',(0.,-0.699524772906136,0.714608348741196));
#23034=DIRECTION('',(0.,-0.754073092756362,0.656790507529498));
#23035=DIRECTION('',(0.,-0.803856860617217,0.594822786751342));
#23036=DIRECTION('',(0.,-0.848561521636558,0.529096724614553));
#23037=DIRECTION('',(0.,-0.887904612902449,0.460027606113537));
#23038=DIRECTION('',(0.,-0.921637548163022,0.388051839083456));
#23039=DIRECTION('',(0.,-0.94954718849933,0.313624196791349));
#23040=DIRECTION('',(0.,-0.275637355817,-0.961261695938319));
#23041=DIRECTION('',(0.,0.923879532511286,-0.382683432365091));
#23042=DIRECTION('',(0.,0.484809620246337,0.874619707139396));
#23043=DIRECTION('',(0.,0.856292125836473,-0.516491815259889));
#23044=DIRECTION('',(0.,0.816221627432192,-0.577738915871126));
#23045=DIRECTION('',(0.,0.771778750427186,-0.635891154513924));
#23046=DIRECTION('',(0.,0.723201568743836,-0.690637018242184));
#23047=DIRECTION('',(0.,0.670750303163526,-0.741683241556689));
#23048=DIRECTION('',(0.,0.614705927362394,-0.788756377385019));
#23049=DIRECTION('',(0.,0.555368662776888,-0.831604261897095));
#23050=DIRECTION('',(0.,0.493056370361895,-0.869997365309547));
#23051=DIRECTION('',(0.,0.428102847856613,-0.90373002144283));
#23052=DIRECTION('',(0.,0.360856041679387,-0.932621529444546));
#23053=DIRECTION('',(0.,0.291676183030194,-0.956517121777199));
#23054=DIRECTION('',(0.,0.220933858185349,-0.975288793285013));
#23055=DIRECTION('',(0.,0.14900802332161,-0.98883598689863));
#23056=DIRECTION('',(0.,0.0762839745039523,-0.997086132304467));
#23057=DIRECTION('',(0.,0.00315128371150461,-0.999995034693158));
#23058=DIRECTION('',(0.,-0.0699982880419509,-0.997547111504613));
#23059=DIRECTION('',(0.,-0.142772889313813,-0.98975547590149));
#23060=DIRECTION('',(0.,-0.214782677322933,-0.976661866523923));
#23061=DIRECTION('',(0.,-0.285641906279744,-0.958336423901791));
#23062=DIRECTION('',(0.,-0.354970993769442,-0.934877314722277));
#23063=DIRECTION('',(0.,-0.422398554118875,-0.906410205965425));
#23064=DIRECTION('',(0.,-0.48756338785468,-0.873087591724717));
#23065=DIRECTION('',(0.,-0.550116416595494,-0.835087976318742));
#23066=DIRECTION('',(0.,-0.609722553013205,-0.792614918069966));
#23067=DIRECTION('',(0.,-0.666062495846262,-0.745895938872875));
#23068=DIRECTION('',(0.,-0.71883444034933,-0.69518130539282));
#23069=DIRECTION('',(0.,-0.767755695016675,-0.640742688424505));
#23070=DIRECTION('',(0.,-0.812564195918805,-0.582871707591668));
#23071=DIRECTION('',(0.,-0.85301991054017,-0.521878369183893));
#23072=DIRECTION('',(0.,-0.888906123597886,-0.458089405498731));
#23073=DIRECTION('',(0.,-0.920030597953456,-0.39184652458508));
#23074=DIRECTION('',(0.,-0.946226604398715,-0.323504579763685));
#23075=DIRECTION('',(0.,-0.967353814799542,-0.253429668730349));
#23076=DIRECTION('',(0.,-0.983299053812935,-0.181997172424701));
#23077=DIRECTION('',(0.,-0.993976905150596,-0.109589744169987));
#23078=DIRECTION('',(0.,-0.999330169141354,-0.0365952598557893));
#23079=DIRECTION('',(0.,-0.999330169141354,0.0365952598557893));
#23080=DIRECTION('',(0.,-0.993976905150596,0.109589744169988));
#23081=DIRECTION('',(0.,-0.983299053812935,0.181997172424701));
#23082=DIRECTION('',(0.,-0.967353814799542,0.253429668730349));
#23083=DIRECTION('',(0.,-0.946226604398715,0.323504579763685));
#23084=DIRECTION('',(0.,-0.920030597953456,0.39184652458508));
#23085=DIRECTION('',(0.,-0.888906123597886,0.458089405498731));
#23086=DIRECTION('',(0.,-0.853019910540169,0.521878369183895));
#23087=DIRECTION('',(0.,-0.812564195918804,0.582871707591668));
#23088=DIRECTION('',(0.,-0.767755695016677,0.640742688424503));
#23089=DIRECTION('',(0.,-0.718834440349327,0.695181305392823));
#23090=DIRECTION('',(0.,-0.666062495846264,0.745895938872873));
#23091=DIRECTION('',(0.,-0.609722553013204,0.792614918069967));
#23092=DIRECTION('',(0.,-0.550116416595493,0.835087976318743));
#23093=DIRECTION('',(0.,-0.487563387854682,0.873087591724716));
#23094=DIRECTION('',(0.,-0.422398554118871,0.906410205965427));
#23095=DIRECTION('',(0.,-0.354970993769443,0.934877314722276));
#23096=DIRECTION('',(0.,-0.285641906279744,0.958336423901791));
#23097=DIRECTION('',(0.,-0.214782677322933,0.976661866523923));
#23098=DIRECTION('',(0.,-0.142772889313813,0.98975547590149));
#23099=DIRECTION('',(0.,-0.069998288041949,0.997547111504613));
#23100=DIRECTION('',(0.,0.00315128371150461,0.999995034693158));
#23101=DIRECTION('',(0.,0.0762839745039533,0.997086132304467));
#23102=DIRECTION('',(0.,0.14900802332161,0.98883598689863));
#23103=DIRECTION('',(0.,0.22093385818535,0.975288793285012));
#23104=DIRECTION('',(0.,0.291676183030194,0.956517121777199));
#23105=DIRECTION('',(0.,0.360856041679385,0.932621529444547));
#23106=DIRECTION('',(0.,0.428102847856614,0.903730021442829));
#23107=DIRECTION('',(0.,0.493056370361897,0.869997365309546));
#23108=DIRECTION('',(0.,0.555368662776888,0.831604261897095));
#23109=DIRECTION('',(0.,0.614705927362395,0.788756377385019));
#23110=DIRECTION('',(0.,0.670750303163526,0.741683241556689));
#23111=DIRECTION('',(0.,0.723201568743836,0.690637018242183));
#23112=DIRECTION('',(0.,0.771778750427187,0.635891154513923));
#23113=DIRECTION('',(0.,0.816221627432192,0.577738915871126));
#23114=DIRECTION('',(0.,0.856292125836473,0.516491815259888));
#23115=DIRECTION('',(0.,0.48480962024634,-0.874619707139394));
#23116=DIRECTION('',(0.,0.923879532511287,0.382683432365089));
#23117=DIRECTION('center_axis',(1.,0.,0.));
#23118=DIRECTION('ref_axis',(0.,0.,-1.));
#23119=DIRECTION('center_axis',(-1.,0.,0.));
#23120=DIRECTION('ref_axis',(0.,0.,-1.));
#23121=DIRECTION('',(0.707106781186547,-8.65956056235494E-17,-0.707106781186548));
#23122=DIRECTION('center_axis',(1.,0.,0.));
#23123=DIRECTION('ref_axis',(0.,0.,-1.));
#23124=DIRECTION('center_axis',(1.,0.,0.));
#23125=DIRECTION('ref_axis',(0.,0.,-1.));
#23126=DIRECTION('',(1.,0.,0.));
#23127=DIRECTION('center_axis',(-1.,0.,0.));
#23128=DIRECTION('ref_axis',(0.,0.,-1.));
#23129=DIRECTION('center_axis',(1.,0.,0.));
#23130=DIRECTION('ref_axis',(0.,0.,-1.));
#23131=DIRECTION('',(-0.707106781186547,8.65956056235494E-17,-0.707106781186548));
#23132=DIRECTION('center_axis',(0.,0.382683432365089,-0.923879532511287));
#23133=DIRECTION('ref_axis',(0.,0.923879532511287,0.382683432365089));
#23134=DIRECTION('',(1.,0.,0.));
#23135=DIRECTION('',(1.,0.,0.));
#23136=DIRECTION('center_axis',(0.,-0.874619707139394,-0.48480962024634));
#23137=DIRECTION('ref_axis',(0.,0.48480962024634,-0.874619707139394));
#23138=DIRECTION('',(1.,0.,0.));
#23139=DIRECTION('center_axis',(0.,0.516491815259888,-0.856292125836473));
#23140=DIRECTION('ref_axis',(0.,0.856292125836473,0.516491815259888));
#23141=DIRECTION('',(1.,0.,0.));
#23142=DIRECTION('center_axis',(0.,0.577738915871126,-0.816221627432192));
#23143=DIRECTION('ref_axis',(0.,0.816221627432192,0.577738915871126));
#23144=DIRECTION('',(1.,0.,0.));
#23145=DIRECTION('center_axis',(0.,0.635891154513923,-0.771778750427187));
#23146=DIRECTION('ref_axis',(0.,0.771778750427187,0.635891154513923));
#23147=DIRECTION('',(1.,0.,0.));
#23148=DIRECTION('center_axis',(0.,0.690637018242184,-0.723201568743836));
#23149=DIRECTION('ref_axis',(0.,0.723201568743836,0.690637018242183));
#23150=DIRECTION('',(1.,0.,0.));
#23151=DIRECTION('center_axis',(0.,0.741683241556689,-0.670750303163526));
#23152=DIRECTION('ref_axis',(0.,0.670750303163526,0.741683241556689));
#23153=DIRECTION('',(1.,0.,0.));
#23154=DIRECTION('center_axis',(0.,0.788756377385019,-0.614705927362395));
#23155=DIRECTION('ref_axis',(0.,0.614705927362395,0.788756377385019));
#23156=DIRECTION('',(1.,0.,0.));
#23157=DIRECTION('center_axis',(0.,0.831604261897095,-0.555368662776888));
#23158=DIRECTION('ref_axis',(0.,0.555368662776888,0.831604261897095));
#23159=DIRECTION('',(1.,0.,0.));
#23160=DIRECTION('center_axis',(0.,0.869997365309546,-0.493056370361897));
#23161=DIRECTION('ref_axis',(0.,0.493056370361897,0.869997365309546));
#23162=DIRECTION('',(1.,0.,0.));
#23163=DIRECTION('center_axis',(0.,0.903730021442829,-0.428102847856614));
#23164=DIRECTION('ref_axis',(0.,0.428102847856614,0.903730021442829));
#23165=DIRECTION('',(1.,0.,0.));
#23166=DIRECTION('center_axis',(0.,0.932621529444547,-0.360856041679385));
#23167=DIRECTION('ref_axis',(0.,0.360856041679385,0.932621529444547));
#23168=DIRECTION('',(1.,0.,0.));
#23169=DIRECTION('center_axis',(0.,0.956517121777199,-0.291676183030194));
#23170=DIRECTION('ref_axis',(0.,0.291676183030194,0.956517121777199));
#23171=DIRECTION('',(1.,0.,0.));
#23172=DIRECTION('center_axis',(0.,0.975288793285012,-0.22093385818535));
#23173=DIRECTION('ref_axis',(0.,0.22093385818535,0.975288793285012));
#23174=DIRECTION('',(1.,0.,0.));
#23175=DIRECTION('center_axis',(0.,0.98883598689863,-0.14900802332161));
#23176=DIRECTION('ref_axis',(0.,0.14900802332161,0.98883598689863));
#23177=DIRECTION('',(1.,0.,0.));
#23178=DIRECTION('center_axis',(0.,0.997086132304467,-0.0762839745039533));
#23179=DIRECTION('ref_axis',(0.,0.0762839745039533,0.997086132304467));
#23180=DIRECTION('',(1.,0.,0.));
#23181=DIRECTION('center_axis',(0.,0.999995034693158,-0.00315128371150461));
#23182=DIRECTION('ref_axis',(0.,0.00315128371150461,0.999995034693158));
#23183=DIRECTION('',(1.,0.,0.));
#23184=DIRECTION('center_axis',(0.,0.997547111504613,0.069998288041949));
#23185=DIRECTION('ref_axis',(0.,-0.069998288041949,0.997547111504613));
#23186=DIRECTION('',(1.,0.,0.));
#23187=DIRECTION('center_axis',(0.,0.98975547590149,0.142772889313813));
#23188=DIRECTION('ref_axis',(0.,-0.142772889313813,0.98975547590149));
#23189=DIRECTION('',(1.,0.,0.));
#23190=DIRECTION('center_axis',(0.,0.976661866523923,0.214782677322933));
#23191=DIRECTION('ref_axis',(0.,-0.214782677322933,0.976661866523923));
#23192=DIRECTION('',(1.,0.,0.));
#23193=DIRECTION('center_axis',(0.,0.958336423901792,0.285641906279744));
#23194=DIRECTION('ref_axis',(0.,-0.285641906279744,0.958336423901791));
#23195=DIRECTION('',(1.,0.,0.));
#23196=DIRECTION('center_axis',(0.,0.934877314722276,0.354970993769443));
#23197=DIRECTION('ref_axis',(0.,-0.354970993769443,0.934877314722276));
#23198=DIRECTION('',(1.,0.,0.));
#23199=DIRECTION('center_axis',(0.,0.906410205965427,0.422398554118871));
#23200=DIRECTION('ref_axis',(0.,-0.422398554118871,0.906410205965427));
#23201=DIRECTION('',(1.,0.,0.));
#23202=DIRECTION('center_axis',(0.,0.873087591724716,0.487563387854682));
#23203=DIRECTION('ref_axis',(0.,-0.487563387854682,0.873087591724716));
#23204=DIRECTION('',(1.,0.,0.));
#23205=DIRECTION('center_axis',(0.,0.835087976318743,0.550116416595493));
#23206=DIRECTION('ref_axis',(0.,-0.550116416595493,0.835087976318743));
#23207=DIRECTION('',(1.,0.,0.));
#23208=DIRECTION('center_axis',(0.,0.792614918069967,0.609722553013204));
#23209=DIRECTION('ref_axis',(0.,-0.609722553013204,0.792614918069967));
#23210=DIRECTION('',(1.,0.,0.));
#23211=DIRECTION('center_axis',(0.,0.745895938872873,0.666062495846264));
#23212=DIRECTION('ref_axis',(0.,-0.666062495846264,0.745895938872873));
#23213=DIRECTION('',(1.,0.,0.));
#23214=DIRECTION('center_axis',(0.,0.695181305392823,0.718834440349327));
#23215=DIRECTION('ref_axis',(0.,-0.718834440349327,0.695181305392823));
#23216=DIRECTION('',(1.,0.,0.));
#23217=DIRECTION('center_axis',(0.,0.640742688424503,0.767755695016677));
#23218=DIRECTION('ref_axis',(0.,-0.767755695016677,0.640742688424503));
#23219=DIRECTION('',(1.,0.,0.));
#23220=DIRECTION('center_axis',(0.,0.582871707591668,0.812564195918804));
#23221=DIRECTION('ref_axis',(0.,-0.812564195918804,0.582871707591668));
#23222=DIRECTION('',(1.,0.,0.));
#23223=DIRECTION('center_axis',(0.,0.521878369183895,0.853019910540169));
#23224=DIRECTION('ref_axis',(0.,-0.853019910540169,0.521878369183895));
#23225=DIRECTION('',(1.,0.,0.));
#23226=DIRECTION('center_axis',(0.,0.458089405498731,0.888906123597886));
#23227=DIRECTION('ref_axis',(0.,-0.888906123597886,0.458089405498731));
#23228=DIRECTION('',(1.,0.,0.));
#23229=DIRECTION('center_axis',(0.,0.39184652458508,0.920030597953456));
#23230=DIRECTION('ref_axis',(0.,-0.920030597953456,0.39184652458508));
#23231=DIRECTION('',(1.,0.,0.));
#23232=DIRECTION('center_axis',(0.,0.323504579763685,0.946226604398715));
#23233=DIRECTION('ref_axis',(0.,-0.946226604398715,0.323504579763685));
#23234=DIRECTION('',(1.,0.,0.));
#23235=DIRECTION('center_axis',(0.,0.253429668730349,0.967353814799542));
#23236=DIRECTION('ref_axis',(0.,-0.967353814799542,0.253429668730349));
#23237=DIRECTION('',(1.,0.,0.));
#23238=DIRECTION('center_axis',(0.,0.181997172424701,0.983299053812935));
#23239=DIRECTION('ref_axis',(0.,-0.983299053812935,0.181997172424701));
#23240=DIRECTION('',(1.,0.,0.));
#23241=DIRECTION('center_axis',(0.,0.109589744169988,0.993976905150596));
#23242=DIRECTION('ref_axis',(0.,-0.993976905150596,0.109589744169988));
#23243=DIRECTION('',(1.,0.,0.));
#23244=DIRECTION('center_axis',(0.,0.0365952598557893,0.999330169141354));
#23245=DIRECTION('ref_axis',(0.,-0.999330169141354,0.0365952598557893));
#23246=DIRECTION('',(1.,0.,0.));
#23247=DIRECTION('center_axis',(0.,-0.0365952598557893,0.999330169141354));
#23248=DIRECTION('ref_axis',(0.,-0.999330169141354,-0.0365952598557893));
#23249=DIRECTION('',(1.,0.,0.));
#23250=DIRECTION('center_axis',(0.,-0.109589744169987,0.993976905150596));
#23251=DIRECTION('ref_axis',(0.,-0.993976905150596,-0.109589744169987));
#23252=DIRECTION('',(1.,0.,0.));
#23253=DIRECTION('center_axis',(0.,-0.181997172424701,0.983299053812935));
#23254=DIRECTION('ref_axis',(0.,-0.983299053812935,-0.181997172424701));
#23255=DIRECTION('',(1.,0.,0.));
#23256=DIRECTION('center_axis',(0.,-0.253429668730349,0.967353814799542));
#23257=DIRECTION('ref_axis',(0.,-0.967353814799542,-0.253429668730349));
#23258=DIRECTION('',(1.,0.,0.));
#23259=DIRECTION('center_axis',(0.,-0.323504579763685,0.946226604398715));
#23260=DIRECTION('ref_axis',(0.,-0.946226604398715,-0.323504579763685));
#23261=DIRECTION('',(1.,0.,0.));
#23262=DIRECTION('center_axis',(0.,-0.39184652458508,0.920030597953456));
#23263=DIRECTION('ref_axis',(0.,-0.920030597953456,-0.39184652458508));
#23264=DIRECTION('',(1.,0.,0.));
#23265=DIRECTION('center_axis',(0.,-0.458089405498731,0.888906123597886));
#23266=DIRECTION('ref_axis',(0.,-0.888906123597886,-0.458089405498731));
#23267=DIRECTION('',(1.,0.,0.));
#23268=DIRECTION('center_axis',(0.,-0.521878369183893,0.85301991054017));
#23269=DIRECTION('ref_axis',(0.,-0.85301991054017,-0.521878369183893));
#23270=DIRECTION('',(1.,0.,0.));
#23271=DIRECTION('center_axis',(0.,-0.582871707591668,0.812564195918805));
#23272=DIRECTION('ref_axis',(0.,-0.812564195918805,-0.582871707591668));
#23273=DIRECTION('',(1.,0.,0.));
#23274=DIRECTION('center_axis',(0.,-0.640742688424505,0.767755695016675));
#23275=DIRECTION('ref_axis',(0.,-0.767755695016675,-0.640742688424505));
#23276=DIRECTION('',(1.,0.,0.));
#23277=DIRECTION('center_axis',(0.,-0.69518130539282,0.71883444034933));
#23278=DIRECTION('ref_axis',(0.,-0.71883444034933,-0.69518130539282));
#23279=DIRECTION('',(1.,0.,0.));
#23280=DIRECTION('center_axis',(0.,-0.745895938872875,0.666062495846262));
#23281=DIRECTION('ref_axis',(0.,-0.666062495846262,-0.745895938872875));
#23282=DIRECTION('',(1.,0.,0.));
#23283=DIRECTION('center_axis',(0.,-0.792614918069966,0.609722553013205));
#23284=DIRECTION('ref_axis',(0.,-0.609722553013205,-0.792614918069966));
#23285=DIRECTION('',(1.,0.,0.));
#23286=DIRECTION('center_axis',(0.,-0.835087976318742,0.550116416595494));
#23287=DIRECTION('ref_axis',(0.,-0.550116416595494,-0.835087976318742));
#23288=DIRECTION('',(1.,0.,0.));
#23289=DIRECTION('center_axis',(0.,-0.873087591724717,0.487563387854681));
#23290=DIRECTION('ref_axis',(0.,-0.487563387854681,-0.873087591724717));
#23291=DIRECTION('',(1.,0.,0.));
#23292=DIRECTION('center_axis',(0.,-0.906410205965425,0.422398554118875));
#23293=DIRECTION('ref_axis',(0.,-0.422398554118875,-0.906410205965425));
#23294=DIRECTION('',(1.,0.,0.));
#23295=DIRECTION('center_axis',(0.,-0.934877314722277,0.354970993769442));
#23296=DIRECTION('ref_axis',(0.,-0.354970993769442,-0.934877314722277));
#23297=DIRECTION('',(1.,0.,0.));
#23298=DIRECTION('center_axis',(0.,-0.958336423901792,0.285641906279744));
#23299=DIRECTION('ref_axis',(0.,-0.285641906279744,-0.958336423901791));
#23300=DIRECTION('',(1.,0.,0.));
#23301=DIRECTION('center_axis',(0.,-0.976661866523923,0.214782677322933));
#23302=DIRECTION('ref_axis',(0.,-0.214782677322933,-0.976661866523923));
#23303=DIRECTION('',(1.,0.,0.));
#23304=DIRECTION('center_axis',(0.,-0.98975547590149,0.142772889313813));
#23305=DIRECTION('ref_axis',(0.,-0.142772889313813,-0.98975547590149));
#23306=DIRECTION('',(1.,0.,0.));
#23307=DIRECTION('center_axis',(0.,-0.997547111504613,0.0699982880419509));
#23308=DIRECTION('ref_axis',(0.,-0.0699982880419509,-0.997547111504613));
#23309=DIRECTION('',(1.,0.,0.));
#23310=DIRECTION('center_axis',(0.,-0.999995034693158,-0.00315128371150461));
#23311=DIRECTION('ref_axis',(0.,0.00315128371150461,-0.999995034693158));
#23312=DIRECTION('',(1.,0.,0.));
#23313=DIRECTION('center_axis',(0.,-0.997086132304467,-0.0762839745039523));
#23314=DIRECTION('ref_axis',(0.,0.0762839745039523,-0.997086132304467));
#23315=DIRECTION('',(1.,0.,0.));
#23316=DIRECTION('center_axis',(0.,-0.98883598689863,-0.14900802332161));
#23317=DIRECTION('ref_axis',(0.,0.14900802332161,-0.98883598689863));
#23318=DIRECTION('',(1.,0.,0.));
#23319=DIRECTION('center_axis',(0.,-0.975288793285013,-0.220933858185349));
#23320=DIRECTION('ref_axis',(0.,0.220933858185349,-0.975288793285013));
#23321=DIRECTION('',(1.,0.,0.));
#23322=DIRECTION('center_axis',(0.,-0.956517121777199,-0.291676183030194));
#23323=DIRECTION('ref_axis',(0.,0.291676183030194,-0.956517121777199));
#23324=DIRECTION('',(1.,0.,0.));
#23325=DIRECTION('center_axis',(0.,-0.932621529444546,-0.360856041679387));
#23326=DIRECTION('ref_axis',(0.,0.360856041679387,-0.932621529444546));
#23327=DIRECTION('',(1.,0.,0.));
#23328=DIRECTION('center_axis',(0.,-0.90373002144283,-0.428102847856613));
#23329=DIRECTION('ref_axis',(0.,0.428102847856613,-0.90373002144283));
#23330=DIRECTION('',(1.,0.,0.));
#23331=DIRECTION('center_axis',(0.,-0.869997365309547,-0.493056370361895));
#23332=DIRECTION('ref_axis',(0.,0.493056370361895,-0.869997365309547));
#23333=DIRECTION('',(1.,0.,0.));
#23334=DIRECTION('center_axis',(0.,-0.831604261897095,-0.555368662776888));
#23335=DIRECTION('ref_axis',(0.,0.555368662776888,-0.831604261897095));
#23336=DIRECTION('',(1.,0.,0.));
#23337=DIRECTION('center_axis',(0.,-0.788756377385019,-0.614705927362394));
#23338=DIRECTION('ref_axis',(0.,0.614705927362394,-0.788756377385019));
#23339=DIRECTION('',(1.,0.,0.));
#23340=DIRECTION('center_axis',(0.,-0.741683241556689,-0.670750303163526));
#23341=DIRECTION('ref_axis',(0.,0.670750303163526,-0.741683241556689));
#23342=DIRECTION('',(1.,0.,0.));
#23343=DIRECTION('center_axis',(0.,-0.690637018242184,-0.723201568743836));
#23344=DIRECTION('ref_axis',(0.,0.723201568743836,-0.690637018242184));
#23345=DIRECTION('',(1.,0.,0.));
#23346=DIRECTION('center_axis',(0.,-0.635891154513924,-0.771778750427186));
#23347=DIRECTION('ref_axis',(0.,0.771778750427186,-0.635891154513924));
#23348=DIRECTION('',(1.,0.,0.));
#23349=DIRECTION('center_axis',(0.,-0.577738915871126,-0.816221627432192));
#23350=DIRECTION('ref_axis',(0.,0.816221627432192,-0.577738915871126));
#23351=DIRECTION('',(1.,0.,0.));
#23352=DIRECTION('center_axis',(0.,-0.516491815259888,-0.856292125836473));
#23353=DIRECTION('ref_axis',(0.,0.856292125836472,-0.516491815259888));
#23354=DIRECTION('',(1.,0.,0.));
#23355=DIRECTION('center_axis',(0.,0.874619707139396,-0.484809620246337));
#23356=DIRECTION('ref_axis',(0.,0.484809620246337,0.874619707139396));
#23357=DIRECTION('',(1.,0.,0.));
#23358=DIRECTION('center_axis',(0.,-0.382683432365091,-0.923879532511286));
#23359=DIRECTION('ref_axis',(0.,0.923879532511286,-0.382683432365091));
#23360=DIRECTION('',(1.,0.,0.));
#23361=DIRECTION('center_axis',(0.,-0.961261695938319,0.275637355817));
#23362=DIRECTION('ref_axis',(0.,-0.275637355817,-0.961261695938319));
#23363=DIRECTION('',(1.,0.,0.));
#23364=DIRECTION('center_axis',(0.,0.313624196791349,0.94954718849933));
#23365=DIRECTION('ref_axis',(0.,-0.94954718849933,0.313624196791349));
#23366=DIRECTION('',(1.,0.,0.));
#23367=DIRECTION('center_axis',(0.,0.388051839083456,0.921637548163023));
#23368=DIRECTION('ref_axis',(0.,-0.921637548163022,0.388051839083456));
#23369=DIRECTION('',(1.,0.,0.));
#23370=DIRECTION('center_axis',(0.,0.460027606113537,0.88790461290245));
#23371=DIRECTION('ref_axis',(0.,-0.887904612902449,0.460027606113537));
#23372=DIRECTION('',(1.,0.,0.));
#23373=DIRECTION('center_axis',(0.,0.529096724614553,0.848561521636558));
#23374=DIRECTION('ref_axis',(0.,-0.848561521636558,0.529096724614553));
#23375=DIRECTION('',(1.,0.,0.));
#23376=DIRECTION('center_axis',(0.,0.594822786751342,0.803856860617217));
#23377=DIRECTION('ref_axis',(0.,-0.803856860617217,0.594822786751342));
#23378=DIRECTION('',(1.,0.,0.));
#23379=DIRECTION('center_axis',(0.,0.656790507529498,0.754073092756362));
#23380=DIRECTION('ref_axis',(0.,-0.754073092756362,0.656790507529498));
#23381=DIRECTION('',(1.,0.,0.));
#23382=DIRECTION('center_axis',(0.,0.714608348741196,0.699524772906136));
#23383=DIRECTION('ref_axis',(0.,-0.699524772906136,0.714608348741196));
#23384=DIRECTION('',(1.,0.,0.));
#23385=DIRECTION('center_axis',(0.,0.767910992868789,0.640556560368615));
#23386=DIRECTION('ref_axis',(0.,-0.640556560368615,0.767910992868789));
#23387=DIRECTION('',(1.,0.,0.));
#23388=DIRECTION('center_axis',(0.,0.816361651315052,0.577541041192885));
#23389=DIRECTION('ref_axis',(0.,-0.577541041192885,0.816361651315052));
#23390=DIRECTION('',(1.,0.,0.));
#23391=DIRECTION('center_axis',(0.,0.85965419237564,0.51087637401918));
#23392=DIRECTION('ref_axis',(0.,-0.51087637401918,0.85965419237564));
#23393=DIRECTION('',(1.,0.,0.));
#23394=DIRECTION('center_axis',(0.,0.897515075508373,0.44098377434459));
#23395=DIRECTION('ref_axis',(0.,-0.44098377434459,0.897515075508373));
#23396=DIRECTION('',(1.,0.,0.));
#23397=DIRECTION('center_axis',(0.,0.929705079677808,0.368304853105793));
#23398=DIRECTION('ref_axis',(0.,-0.368304853105793,0.929705079677808));
#23399=DIRECTION('',(1.,0.,0.));
#23400=DIRECTION('center_axis',(0.,0.95602081485468,0.293298826394844));
#23401=DIRECTION('ref_axis',(0.,-0.293298826394844,0.95602081485468));
#23402=DIRECTION('',(1.,0.,0.));
#23403=DIRECTION('center_axis',(0.,0.976296007119934,0.2164396139381));
#23404=DIRECTION('ref_axis',(0.,-0.2164396139381,0.976296007119934));
#23405=DIRECTION('',(1.,0.,0.));
#23406=DIRECTION('center_axis',(0.,0.990402549253496,0.138212844671456));
#23407=DIRECTION('ref_axis',(0.,-0.138212844671456,0.990402549253496));
#23408=DIRECTION('',(1.,0.,0.));
#23409=DIRECTION('center_axis',(0.,0.998251310169761,0.0591127883317614));
#23410=DIRECTION('ref_axis',(0.,-0.0591127883317614,0.998251310169761));
#23411=DIRECTION('',(1.,0.,0.));
#23412=DIRECTION('center_axis',(0.,0.999792698085388,-0.0203607675478923));
#23413=DIRECTION('ref_axis',(0.,0.0203607675478923,0.999792698085389));
#23414=DIRECTION('',(1.,0.,0.));
#23415=DIRECTION('center_axis',(0.,0.995016973861122,-0.0997056755067372));
#23416=DIRECTION('ref_axis',(0.,0.0997056755067372,0.995016973861122));
#23417=DIRECTION('',(1.,0.,0.));
#23418=DIRECTION('center_axis',(0.,0.983954312537781,-0.178420600935832));
#23419=DIRECTION('ref_axis',(0.,0.178420600935832,0.983954312537781));
#23420=DIRECTION('',(1.,0.,0.));
#23421=DIRECTION('center_axis',(0.,0.966674612677614,-0.256008189721705));
#23422=DIRECTION('ref_axis',(0.,0.256008189721705,0.966674612677614));
#23423=DIRECTION('',(1.,0.,0.));
#23424=DIRECTION('center_axis',(0.,0.943287054715696,-0.331978210739482));
#23425=DIRECTION('ref_axis',(0.,0.331978210739482,0.943287054715696));
#23426=DIRECTION('',(1.,0.,0.));
#23427=DIRECTION('center_axis',(0.,0.913939411111865,-0.405850653339991));
#23428=DIRECTION('ref_axis',(0.,0.405850653339991,0.913939411111865));
#23429=DIRECTION('',(1.,0.,0.));
#23430=DIRECTION('center_axis',(0.,0.878817112661964,-0.47715876025961));
#23431=DIRECTION('ref_axis',(0.,0.47715876025961,0.878817112661964));
#23432=DIRECTION('',(1.,0.,0.));
#23433=DIRECTION('center_axis',(0.,0.83814207686784,-0.545451976789583));
#23434=DIRECTION('ref_axis',(0.,0.545451976789583,0.83814207686784));
#23435=DIRECTION('',(1.,0.,0.));
#23436=DIRECTION('center_axis',(0.,0.792171305768909,-0.610298797570814));
#23437=DIRECTION('ref_axis',(0.,0.610298797570814,0.792171305768909));
#23438=DIRECTION('',(1.,0.,0.));
#23439=DIRECTION('center_axis',(0.,0.741195262094844,-0.671289493026783));
#23440=DIRECTION('ref_axis',(0.,0.671289493026783,0.741195262094844));
#23441=DIRECTION('',(1.,0.,0.));
#23442=DIRECTION('center_axis',(0.,0.685536033999469,-0.728038698207918));
#23443=DIRECTION('ref_axis',(0.,0.728038698207918,0.685536033999469));
#23444=DIRECTION('',(1.,0.,0.));
#23445=DIRECTION('center_axis',(0.,0.62554529997191,-0.780187847689935));
#23446=DIRECTION('ref_axis',(0.,0.780187847689935,0.62554529997191));
#23447=DIRECTION('',(1.,0.,0.));
#23448=DIRECTION('center_axis',(0.,0.561602106783492,-0.827407441141511));
#23449=DIRECTION('ref_axis',(0.,0.827407441141511,0.561602106783492));
#23450=DIRECTION('',(1.,0.,0.));
#23451=DIRECTION('center_axis',(0.,0.494110474510307,-0.869399125246396));
#23452=DIRECTION('ref_axis',(0.,0.869399125246396,0.494110474510307));
#23453=DIRECTION('',(1.,0.,0.));
#23454=DIRECTION('center_axis',(0.,0.423496843763887,-0.905897578825568));
#23455=DIRECTION('ref_axis',(0.,0.905897578825568,0.423496843763887));
#23456=DIRECTION('',(1.,0.,0.));
#23457=DIRECTION('center_axis',(0.,0.350207381259467,-0.936672189248398));
#23458=DIRECTION('ref_axis',(0.,0.936672189248398,0.350207381259467));
#23459=DIRECTION('',(1.,0.,0.));
#23460=DIRECTION('center_axis',(0.,0.274705160746442,-0.96152850954055));
#23461=DIRECTION('ref_axis',(0.,0.96152850954055,0.274705160746442));
#23462=DIRECTION('',(1.,0.,0.));
#23463=DIRECTION('center_axis',(0.,0.197467237112997,-0.980309486982024));
#23464=DIRECTION('ref_axis',(0.,0.980309486982024,0.197467237112997));
#23465=DIRECTION('',(1.,0.,0.));
#23466=DIRECTION('center_axis',(0.,0.118981632152029,-0.992896455432509));
#23467=DIRECTION('ref_axis',(0.,0.992896455432508,0.118981632152029));
#23468=DIRECTION('',(1.,0.,0.));
#23469=DIRECTION('center_axis',(0.,0.0397442510335229,-0.999209885114126));
#23470=DIRECTION('ref_axis',(0.,0.999209885114126,0.0397442510335229));
#23471=DIRECTION('',(1.,0.,0.));
#23472=DIRECTION('center_axis',(0.,-0.0397442510335258,-0.999209885114126));
#23473=DIRECTION('ref_axis',(0.,0.999209885114126,-0.0397442510335258));
#23474=DIRECTION('',(1.,0.,0.));
#23475=DIRECTION('center_axis',(0.,-0.118981632152026,-0.992896455432509));
#23476=DIRECTION('ref_axis',(0.,0.992896455432509,-0.118981632152026));
#23477=DIRECTION('',(1.,0.,0.));
#23478=DIRECTION('center_axis',(0.,-0.197467237112996,-0.980309486982024));
#23479=DIRECTION('ref_axis',(0.,0.980309486982024,-0.197467237112996));
#23480=DIRECTION('',(1.,0.,0.));
#23481=DIRECTION('center_axis',(0.,-0.274705160746445,-0.961528509540549));
#23482=DIRECTION('ref_axis',(0.,0.961528509540549,-0.274705160746445));
#23483=DIRECTION('',(1.,0.,0.));
#23484=DIRECTION('center_axis',(0.,-0.350207381259469,-0.936672189248397));
#23485=DIRECTION('ref_axis',(0.,0.936672189248397,-0.350207381259469));
#23486=DIRECTION('',(1.,0.,0.));
#23487=DIRECTION('center_axis',(0.,-0.423496843763883,-0.90589757882557));
#23488=DIRECTION('ref_axis',(0.,0.905897578825569,-0.423496843763883));
#23489=DIRECTION('',(1.,0.,0.));
#23490=DIRECTION('center_axis',(0.,-0.494110474510309,-0.869399125246396));
#23491=DIRECTION('ref_axis',(0.,0.869399125246396,-0.494110474510309));
#23492=DIRECTION('',(1.,0.,0.));
#23493=DIRECTION('center_axis',(0.,-0.561602106783492,-0.827407441141511));
#23494=DIRECTION('ref_axis',(0.,0.827407441141511,-0.561602106783492));
#23495=DIRECTION('',(1.,0.,0.));
#23496=DIRECTION('center_axis',(0.,-0.62554529997191,-0.780187847689935));
#23497=DIRECTION('ref_axis',(0.,0.780187847689935,-0.62554529997191));
#23498=DIRECTION('',(1.,0.,0.));
#23499=DIRECTION('center_axis',(0.,-0.685536033999469,-0.728038698207917));
#23500=DIRECTION('ref_axis',(0.,0.728038698207917,-0.685536033999469));
#23501=DIRECTION('',(1.,0.,0.));
#23502=DIRECTION('center_axis',(0.,-0.741195262094845,-0.671289493026783));
#23503=DIRECTION('ref_axis',(0.,0.671289493026782,-0.741195262094845));
#23504=DIRECTION('',(1.,0.,0.));
#23505=DIRECTION('center_axis',(0.,-0.79217130576891,-0.610298797570813));
#23506=DIRECTION('ref_axis',(0.,0.610298797570813,-0.79217130576891));
#23507=DIRECTION('',(1.,0.,0.));
#23508=DIRECTION('center_axis',(0.,-0.838142076867841,-0.545451976789582));
#23509=DIRECTION('ref_axis',(0.,0.545451976789582,-0.83814207686784));
#23510=DIRECTION('',(1.,0.,0.));
#23511=DIRECTION('center_axis',(0.,-0.878817112661967,-0.477158760259606));
#23512=DIRECTION('ref_axis',(0.,0.477158760259606,-0.878817112661967));
#23513=DIRECTION('',(1.,0.,0.));
#23514=DIRECTION('center_axis',(0.,-0.913939411111864,-0.405850653339993));
#23515=DIRECTION('ref_axis',(0.,0.405850653339993,-0.913939411111864));
#23516=DIRECTION('',(1.,0.,0.));
#23517=DIRECTION('center_axis',(0.,-0.943287054715697,-0.33197821073948));
#23518=DIRECTION('ref_axis',(0.,0.33197821073948,-0.943287054715696));
#23519=DIRECTION('',(1.,0.,0.));
#23520=DIRECTION('center_axis',(0.,-0.966674612677614,-0.256008189721705));
#23521=DIRECTION('ref_axis',(0.,0.256008189721705,-0.966674612677614));
#23522=DIRECTION('',(1.,0.,0.));
#23523=DIRECTION('center_axis',(0.,-0.983954312537781,-0.178420600935832));
#23524=DIRECTION('ref_axis',(0.,0.178420600935832,-0.983954312537781));
#23525=DIRECTION('',(1.,0.,0.));
#23526=DIRECTION('center_axis',(0.,-0.995016973861122,-0.0997056755067357));
#23527=DIRECTION('ref_axis',(0.,0.0997056755067357,-0.995016973861122));
#23528=DIRECTION('',(1.,0.,0.));
#23529=DIRECTION('center_axis',(0.,-0.999792698085388,-0.0203607675478923));
#23530=DIRECTION('ref_axis',(0.,0.0203607675478923,-0.999792698085389));
#23531=DIRECTION('',(1.,0.,0.));
#23532=DIRECTION('center_axis',(0.,-0.998251310169761,0.0591127883317644));
#23533=DIRECTION('ref_axis',(0.,-0.0591127883317644,-0.998251310169761));
#23534=DIRECTION('',(1.,0.,0.));
#23535=DIRECTION('center_axis',(0.,-0.990402549253497,0.138212844671453));
#23536=DIRECTION('ref_axis',(0.,-0.138212844671453,-0.990402549253497));
#23537=DIRECTION('',(1.,0.,0.));
#23538=DIRECTION('center_axis',(0.,-0.976296007119933,0.216439613938106));
#23539=DIRECTION('ref_axis',(0.,-0.216439613938106,-0.976296007119933));
#23540=DIRECTION('',(1.,0.,0.));
#23541=DIRECTION('center_axis',(0.,-0.956020814854681,0.293298826394842));
#23542=DIRECTION('ref_axis',(0.,-0.293298826394842,-0.956020814854681));
#23543=DIRECTION('',(1.,0.,0.));
#23544=DIRECTION('center_axis',(0.,-0.929705079677808,0.368304853105795));
#23545=DIRECTION('ref_axis',(0.,-0.368304853105795,-0.929705079677808));
#23546=DIRECTION('',(1.,0.,0.));
#23547=DIRECTION('center_axis',(0.,-0.897515075508373,0.44098377434459));
#23548=DIRECTION('ref_axis',(0.,-0.44098377434459,-0.897515075508373));
#23549=DIRECTION('',(1.,0.,0.));
#23550=DIRECTION('center_axis',(0.,-0.85965419237564,0.510876374019181));
#23551=DIRECTION('ref_axis',(0.,-0.510876374019181,-0.85965419237564));
#23552=DIRECTION('',(1.,0.,0.));
#23553=DIRECTION('center_axis',(0.,-0.816361651315051,0.577541041192886));
#23554=DIRECTION('ref_axis',(0.,-0.577541041192886,-0.816361651315051));
#23555=DIRECTION('',(1.,0.,0.));
#23556=DIRECTION('center_axis',(0.,-0.767910992868789,0.640556560368615));
#23557=DIRECTION('ref_axis',(0.,-0.640556560368615,-0.767910992868789));
#23558=DIRECTION('',(1.,0.,0.));
#23559=DIRECTION('center_axis',(0.,-0.714608348741195,0.699524772906137));
#23560=DIRECTION('ref_axis',(0.,-0.699524772906137,-0.714608348741195));
#23561=DIRECTION('',(1.,0.,0.));
#23562=DIRECTION('center_axis',(0.,-0.656790507529498,0.754073092756361));
#23563=DIRECTION('ref_axis',(0.,-0.754073092756361,-0.656790507529498));
#23564=DIRECTION('',(1.,0.,0.));
#23565=DIRECTION('center_axis',(0.,-0.59482278675134,0.803856860617219));
#23566=DIRECTION('ref_axis',(0.,-0.803856860617218,-0.59482278675134));
#23567=DIRECTION('',(1.,0.,0.));
#23568=DIRECTION('center_axis',(0.,-0.529096724614554,0.848561521636558));
#23569=DIRECTION('ref_axis',(0.,-0.848561521636558,-0.529096724614554));
#23570=DIRECTION('',(1.,0.,0.));
#23571=DIRECTION('center_axis',(0.,-0.460027606113536,0.88790461290245));
#23572=DIRECTION('ref_axis',(0.,-0.88790461290245,-0.460027606113536));
#23573=DIRECTION('',(1.,0.,0.));
#23574=DIRECTION('center_axis',(0.,-0.388051839083455,0.921637548163023));
#23575=DIRECTION('ref_axis',(0.,-0.921637548163023,-0.388051839083454));
#23576=DIRECTION('',(1.,0.,0.));
#23577=DIRECTION('center_axis',(0.,-0.313624196791348,0.94954718849933));
#23578=DIRECTION('ref_axis',(0.,-0.94954718849933,-0.313624196791348));
#23579=DIRECTION('',(1.,0.,0.));
#23580=DIRECTION('center_axis',(0.,0.961261695938319,0.275637355816999));
#23581=DIRECTION('ref_axis',(0.,-0.275637355816999,0.961261695938319));
#59397=CARTESIAN_POINT('',(0.,0.,0.));
#59398=CARTESIAN_POINT('Origin',(0.1,-2.88925991435643,6.97529047046021));
#59399=CARTESIAN_POINT('',(0.,-2.88925991435643,7.72529047046022));
#59400=CARTESIAN_POINT('Origin',(0.,-2.88925991435643,6.97529047046021));
#59401=CARTESIAN_POINT('',(0.2,-2.88925991435643,7.52529047046021));
#59402=CARTESIAN_POINT('',(0.1,-2.88925991435643,7.62529047046022));
#59403=CARTESIAN_POINT('Origin',(0.2,-2.88925991435643,6.97529047046021));
#59404=CARTESIAN_POINT('Origin',(0.,-2.88925991435643,6.97529047046021));
#59405=CARTESIAN_POINT('',(0.8,-2.88925991435643,7.52529047046021));
#59406=CARTESIAN_POINT('',(0.,-2.88925991435643,7.52529047046021));
#59407=CARTESIAN_POINT('Origin',(0.8,-2.88925991435643,6.97529047046021));
#59408=CARTESIAN_POINT('Origin',(0.,0.,-0.183038486691444));
#59409=CARTESIAN_POINT('',(0.,-1.84677028397389,6.44045336278674));
#59410=CARTESIAN_POINT('',(0.,-2.60477301247064,9.08392302661711));
#59411=CARTESIAN_POINT('',(0.,-1.84677028397389,6.44045336278674));
#59412=CARTESIAN_POINT('',(0.,-3.24822445565046,5.85995203783395));
#59413=CARTESIAN_POINT('',(0.,-3.24822445565046,5.85995203783395));
#59414=CARTESIAN_POINT('',(0.,-3.8784769619707,6.99695765711517));
#59415=CARTESIAN_POINT('',(0.,-3.8784769619707,6.99695765711517));
#59416=CARTESIAN_POINT('',(0.,-4.37985668768992,6.69453922202999));
#59417=CARTESIAN_POINT('',(0.,-4.37985668768992,6.69453922202999));
#59418=CARTESIAN_POINT('',(0.,-4.85777416858265,6.3562591299483));
#59419=CARTESIAN_POINT('',(0.,-4.85777416858265,6.3562591299483));
#59420=CARTESIAN_POINT('',(0.,-5.30966927135158,5.98392949731736));
#59421=CARTESIAN_POINT('',(0.,-5.30966927135158,5.98392949731736));
#59422=CARTESIAN_POINT('',(0.,-5.73312126073229,5.57954483893977));
#59423=CARTESIAN_POINT('',(0.,-5.73312126073229,5.57954483893977));
#59424=CARTESIAN_POINT('',(0.,-6.12586176701418,5.14527138365256));
#59425=CARTESIAN_POINT('',(0.,-6.12586176701418,5.14527138365256));
#59426=CARTESIAN_POINT('',(0.,-6.4857869373617,4.68343547015952));
#59427=CARTESIAN_POINT('',(0.,-6.4857869373617,4.68343547015952));
#59428=CARTESIAN_POINT('',(0.,-6.81096870584301,4.19651108517864));
#59429=CARTESIAN_POINT('',(0.,-6.81096870584301,4.19651108517864));
#59430=CARTESIAN_POINT('',(0.,-7.09966512179413,3.68710661066098));
#59431=CARTESIAN_POINT('',(0.,-7.09966512179413,3.68710661066098));
#59432=CARTESIAN_POINT('',(0.,-7.35032968119119,3.15795085107414));
#59433=CARTESIAN_POINT('',(0.,-7.35032968119119,3.15795085107414));
#59434=CARTESIAN_POINT('',(0.,-7.5616196110438,2.61187841560012));
#59435=CARTESIAN_POINT('',(0.,-7.5616196110438,2.61187841560012));
#59436=CARTESIAN_POINT('',(0.,-7.73240306243155,2.05181453355296));
#59437=CARTESIAN_POINT('',(0.,-7.73240306243155,2.05181453355296));
#59438=CARTESIAN_POINT('',(0.,-7.86176517365131,1.48075938435772));
#59439=CARTESIAN_POINT('',(0.,-7.86176517365131,1.48075938435772));
#59440=CARTESIAN_POINT('',(0.,-7.94901297099613,0.901772026032757));
#59441=CARTESIAN_POINT('',(0.,-7.94901297099613,0.901772026032757));
#59442=CARTESIAN_POINT('',(0.,-7.99367908091301,0.317954008268197));
#59443=CARTESIAN_POINT('',(0.,-7.99367908091301,0.317954008268197));
#59444=CARTESIAN_POINT('',(0.,-7.99552423365383,-0.267567242117311));
#59445=CARTESIAN_POINT('',(0.,-7.99552423365383,-0.267567242117311));
#59446=CARTESIAN_POINT('',(0.,-7.95453854500815,-0.85165517433975));
#59447=CARTESIAN_POINT('',(0.,-7.95453854500815,-0.85165517433975));
#59448=CARTESIAN_POINT('',(0.,-7.87094156925134,-1.43118091568862));
#59449=CARTESIAN_POINT('',(0.,-7.87094156925134,-1.43118091568862));
#59450=CARTESIAN_POINT('',(0.,-7.74518112302486,-2.00304003243553));
#59451=CARTESIAN_POINT('',(0.,-7.74518112302486,-2.00304003243553));
#59452=CARTESIAN_POINT('',(0.,-7.5779308864487,-2.56416915982678));
#59453=CARTESIAN_POINT('',(0.,-7.5779308864487,-2.56416915982678));
#59454=CARTESIAN_POINT('',(0.,-7.37008679431654,-3.11156241207547));
#59455=CARTESIAN_POINT('',(0.,-7.37008679431654,-3.11156241207547));
#59456=CARTESIAN_POINT('',(0.,-7.12276223670551,-3.64228748444736));
#59457=CARTESIAN_POINT('',(0.,-7.12276223670551,-3.64228748444736));
#59458=CARTESIAN_POINT('',(0.,-6.83728209471014,-4.15350136118385));
#59459=CARTESIAN_POINT('',(0.,-6.83728209471014,-4.15350136118385));
#59460=CARTESIAN_POINT('',(0.,-6.51517564325019,-4.64246554511711));
#59461=CARTESIAN_POINT('',(0.,-6.51517564325019,-4.64246554511711));
#59462=CARTESIAN_POINT('',(0.,-6.15816835897094,-5.10656072739463));
#59463=CARTESIAN_POINT('',(0.,-6.15816835897094,-5.10656072739463));
#59464=CARTESIAN_POINT('',(0.,-5.76817267711992,-5.54330081872951));
#59465=CARTESIAN_POINT('',(0.,-5.76817267711992,-5.54330081872951));
#59466=CARTESIAN_POINT('',(0.,-5.34727774691394,-5.95034626701329));
#59467=CARTESIAN_POINT('',(0.,-5.34727774691394,-5.95034626701329));
#59468=CARTESIAN_POINT('',(0.,-4.89773824027559,-6.32551658995075));
#59469=CARTESIAN_POINT('',(0.,-4.89773824027559,-6.32551658995075));
#59470=CARTESIAN_POINT('',(0.,-4.42196227388907,-6.66680205558121));
#59471=CARTESIAN_POINT('',(0.,-4.42196227388907,-6.66680205558121));
#59472=CARTESIAN_POINT('',(0.,-3.922498509275,-6.9723744481156));
#59473=CARTESIAN_POINT('',(0.,-3.922498509275,-6.9723744481156));
#59474=CARTESIAN_POINT('',(0.,-3.40202249998754,-7.24059686141816));
#59475=CARTESIAN_POINT('',(0.,-3.40202249998754,-7.24059686141816));
#59476=CARTESIAN_POINT('',(0.,-2.86332235906941,-7.47003246767062));
#59477=CARTESIAN_POINT('',(0.,-2.86332235906941,-7.47003246767062));
#59478=CARTESIAN_POINT('',(0.,-2.30928382354251,-7.65945221424645));
#59479=CARTESIAN_POINT('',(0.,-2.30928382354251,-7.65945221424645));
#59480=CARTESIAN_POINT('',(0.,-1.74287479594128,-7.80784140756411));
#59481=CARTESIAN_POINT('',(0.,-1.74287479594128,-7.80784140756411));
#59482=CARTESIAN_POINT('',(0.,-1.16712944569752,-7.91440514865052));
#59483=CARTESIAN_POINT('',(0.,-1.16712944569752,-7.91440514865052));
#59484=CARTESIAN_POINT('',(0.,-0.585131955543311,-7.9785725912974));
#59485=CARTESIAN_POINT('',(0.,-0.585131955543311,-7.9785725912974));
#59486=CARTESIAN_POINT('',(0.,-1.46957615897682E-15,-8.));
#59487=CARTESIAN_POINT('',(0.,-1.46957615897682E-15,-8.));
#59488=CARTESIAN_POINT('',(0.,0.585131955543308,-7.9785725912974));
#59489=CARTESIAN_POINT('',(0.,0.585131955543308,-7.9785725912974));
#59490=CARTESIAN_POINT('',(0.,1.16712944569752,-7.91440514865052));
#59491=CARTESIAN_POINT('',(0.,1.16712944569752,-7.91440514865052));
#59492=CARTESIAN_POINT('',(0.,1.74287479594128,-7.80784140756411));
#59493=CARTESIAN_POINT('',(0.,1.74287479594128,-7.80784140756411));
#59494=CARTESIAN_POINT('',(0.,2.30928382354251,-7.65945221424645));
#59495=CARTESIAN_POINT('',(0.,2.30928382354251,-7.65945221424645));
#59496=CARTESIAN_POINT('',(0.,2.86332235906941,-7.47003246767062));
#59497=CARTESIAN_POINT('',(0.,2.86332235906941,-7.47003246767062));
#59498=CARTESIAN_POINT('',(0.,3.40202249998754,-7.24059686141816));
#59499=CARTESIAN_POINT('',(0.,3.40202249998754,-7.24059686141816));
#59500=CARTESIAN_POINT('',(0.,3.922498509275,-6.97237444811561));
#59501=CARTESIAN_POINT('',(0.,3.922498509275,-6.97237444811561));
#59502=CARTESIAN_POINT('',(0.,4.42196227388906,-6.66680205558121));
#59503=CARTESIAN_POINT('',(0.,4.42196227388906,-6.66680205558121));
#59504=CARTESIAN_POINT('',(0.,4.89773824027559,-6.32551658995075));
#59505=CARTESIAN_POINT('',(0.,4.89773824027559,-6.32551658995075));
#59506=CARTESIAN_POINT('',(0.,5.34727774691393,-5.95034626701329));
#59507=CARTESIAN_POINT('',(0.,5.34727774691393,-5.95034626701329));
#59508=CARTESIAN_POINT('',(0.,5.76817267711992,-5.54330081872951));
#59509=CARTESIAN_POINT('',(0.,5.76817267711992,-5.54330081872951));
#59510=CARTESIAN_POINT('',(0.,6.15816835897094,-5.10656072739463));
#59511=CARTESIAN_POINT('',(0.,6.15816835897094,-5.10656072739463));
#59512=CARTESIAN_POINT('',(0.,6.51517564325019,-4.64246554511711));
#59513=CARTESIAN_POINT('',(0.,6.51517564325019,-4.64246554511711));
#59514=CARTESIAN_POINT('',(0.,6.83728209471014,-4.15350136118385));
#59515=CARTESIAN_POINT('',(0.,6.83728209471014,-4.15350136118385));
#59516=CARTESIAN_POINT('',(0.,7.12276223670551,-3.64228748444737));
#59517=CARTESIAN_POINT('',(0.,7.12276223670551,-3.64228748444737));
#59518=CARTESIAN_POINT('',(0.,7.37008679431654,-3.11156241207547));
#59519=CARTESIAN_POINT('',(0.,7.37008679431654,-3.11156241207547));
#59520=CARTESIAN_POINT('',(0.,7.5779308864487,-2.56416915982678));
#59521=CARTESIAN_POINT('',(0.,7.5779308864487,-2.56416915982678));
#59522=CARTESIAN_POINT('',(0.,7.74518112302486,-2.00304003243554));
#59523=CARTESIAN_POINT('',(0.,7.74518112302486,-2.00304003243554));
#59524=CARTESIAN_POINT('',(0.,7.87094156925134,-1.43118091568862));
#59525=CARTESIAN_POINT('',(0.,7.87094156925134,-1.43118091568862));
#59526=CARTESIAN_POINT('',(0.,7.95453854500815,-0.851655174339752));
#59527=CARTESIAN_POINT('',(0.,7.95453854500815,-0.851655174339752));
#59528=CARTESIAN_POINT('',(0.,7.99552423365383,-0.267567242117314));
#59529=CARTESIAN_POINT('',(0.,7.99552423365383,-0.267567242117314));
#59530=CARTESIAN_POINT('',(0.,7.99367908091301,0.317954008268194));
#59531=CARTESIAN_POINT('',(0.,7.99367908091301,0.317954008268194));
#59532=CARTESIAN_POINT('',(0.,7.94901297099613,0.901772026032747));
#59533=CARTESIAN_POINT('',(0.,7.94901297099613,0.901772026032747));
#59534=CARTESIAN_POINT('',(0.,7.86176517365131,1.48075938435771));
#59535=CARTESIAN_POINT('',(0.,7.86176517365131,1.48075938435771));
#59536=CARTESIAN_POINT('',(0.,7.73240306243155,2.05181453355297));
#59537=CARTESIAN_POINT('',(0.,7.73240306243155,2.05181453355297));
#59538=CARTESIAN_POINT('',(0.,7.5616196110438,2.61187841560012));
#59539=CARTESIAN_POINT('',(0.,7.5616196110438,2.61187841560012));
#59540=CARTESIAN_POINT('',(0.,7.35032968119119,3.15795085107413));
#59541=CARTESIAN_POINT('',(0.,7.35032968119119,3.15795085107413));
#59542=CARTESIAN_POINT('',(0.,7.09966512179414,3.68710661066097));
#59543=CARTESIAN_POINT('',(0.,7.09966512179414,3.68710661066097));
#59544=CARTESIAN_POINT('',(0.,6.81096870584301,4.19651108517863));
#59545=CARTESIAN_POINT('',(0.,6.81096870584301,4.19651108517863));
#59546=CARTESIAN_POINT('',(0.,6.4857869373617,4.68343547015952));
#59547=CARTESIAN_POINT('',(0.,6.4857869373617,4.68343547015952));
#59548=CARTESIAN_POINT('',(0.,6.12586176701418,5.14527138365256));
#59549=CARTESIAN_POINT('',(0.,6.12586176701418,5.14527138365256));
#59550=CARTESIAN_POINT('',(0.,5.73312126073229,5.57954483893976));
#59551=CARTESIAN_POINT('',(0.,5.73312126073229,5.57954483893976));
#59552=CARTESIAN_POINT('',(0.,5.30966927135158,5.98392949731736));
#59553=CARTESIAN_POINT('',(0.,5.30966927135158,5.98392949731736));
#59554=CARTESIAN_POINT('',(0.,4.85777416858264,6.35625912994831));
#59555=CARTESIAN_POINT('',(0.,4.85777416858264,6.35625912994831));
#59556=CARTESIAN_POINT('',(0.,4.37985668768992,6.69453922202999));
#59557=CARTESIAN_POINT('',(0.,4.37985668768992,6.69453922202999));
#59558=CARTESIAN_POINT('',(0.,3.8784769619707,6.99695765711516));
#59559=CARTESIAN_POINT('',(0.,3.8784769619707,6.99695765711516));
#59560=CARTESIAN_POINT('',(0.,3.24822445565046,5.85995203783395));
#59561=CARTESIAN_POINT('',(0.,3.24822445565046,5.85995203783395));
#59562=CARTESIAN_POINT('',(0.,1.8467702839739,6.44045336278674));
#59563=CARTESIAN_POINT('',(0.,1.8467702839739,6.44045336278674));
#59564=CARTESIAN_POINT('',(0.,2.60477301247065,9.08392302661711));
#59565=CARTESIAN_POINT('',(0.,2.60477301247065,9.08392302661711));
#59566=CARTESIAN_POINT('',(0.,3.31804090301786,8.84833908515606));
#59567=CARTESIAN_POINT('',(0.,3.31804090301786,8.84833908515606));
#59568=CARTESIAN_POINT('',(0.,4.0103440110564,8.5568476037022));
#59569=CARTESIAN_POINT('',(0.,4.0103440110564,8.5568476037022));
#59570=CARTESIAN_POINT('',(0.,4.67730807342487,8.21129034843334));
#59571=CARTESIAN_POINT('',(0.,4.67730807342487,8.21129034843334));
#59572=CARTESIAN_POINT('',(0.,5.31471892974448,7.81385069589992));
#59573=CARTESIAN_POINT('',(0.,5.31471892974448,7.81385069589992));
#59574=CARTESIAN_POINT('',(0.,5.91854914926258,7.36703983753062));
#59575=CARTESIAN_POINT('',(0.,5.91854914926258,7.36703983753062));
#59576=CARTESIAN_POINT('',(0.,6.48498347785954,6.87368091286531));
#59577=CARTESIAN_POINT('',(0.,6.48498347785954,6.87368091286531));
#59578=CARTESIAN_POINT('',(0.,7.01044294443415,6.33689117176818));
#59579=CARTESIAN_POINT('',(0.,7.01044294443415,6.33689117176818));
#59580=CARTESIAN_POINT('',(0.,7.49160747435326,5.76006227832775));
#59581=CARTESIAN_POINT('',(0.,7.49160747435326,5.76006227832775));
#59582=CARTESIAN_POINT('',(0.,7.92543686708426,5.146838880892));
#59583=CARTESIAN_POINT('',(0.,7.92543686708426,5.146838880892));
#59584=CARTESIAN_POINT('',(0.,8.30919000546483,4.5010955836422));
#59585=CARTESIAN_POINT('',(0.,8.30919000546483,4.5010955836422));
#59586=CARTESIAN_POINT('',(0.,8.6404421752379,3.82691246520876));
#59587=CARTESIAN_POINT('',(0.,8.6404421752379,3.82691246520876));
#59588=CARTESIAN_POINT('',(0.,8.91710038541937,3.12854929901285));
#59589=CARTESIAN_POINT('',(0.,8.91710038541937,3.12854929901285));
#59590=CARTESIAN_POINT('',(0.,9.13741659269838,2.41041863822041));
#59591=CARTESIAN_POINT('',(0.,9.13741659269838,2.41041863822041));
#59592=CARTESIAN_POINT('',(0.,9.29999874631253,1.67705793536937));
#59593=CARTESIAN_POINT('',(0.,9.29999874631253,1.67705793536937));
#59594=CARTESIAN_POINT('',(0.,9.40381958361198,0.933100872829846));
#59595=CARTESIAN_POINT('',(0.,9.40381958361198,0.933100872829846));
#59596=CARTESIAN_POINT('',(0.,9.44822312073834,0.183248085243736));
#59597=CARTESIAN_POINT('',(0.,9.44822312073834,0.183248085243736));
#59598=CARTESIAN_POINT('',(0.,9.43292879740749,-0.567762541068464));
#59599=CARTESIAN_POINT('',(0.,9.43292879740749,-0.567762541068464));
#59600=CARTESIAN_POINT('',(0.,9.35803324960784,-1.31518580407262));
#59601=CARTESIAN_POINT('',(0.,9.35803324960784,-1.31518580407262));
#59602=CARTESIAN_POINT('',(0.,9.22400969901338,-2.05429916820971));
#59603=CARTESIAN_POINT('',(0.,9.22400969901338,-2.05429916820971));
#59604=CARTESIAN_POINT('',(0.,9.03170496296946,-2.7804326033682));
#59605=CARTESIAN_POINT('',(0.,9.03170496296946,-2.7804326033682));
#59606=CARTESIAN_POINT('',(0.,8.78233410394347,-3.48899809210487));
#59607=CARTESIAN_POINT('',(0.,8.78233410394347,-3.48899809210487));
#59608=CARTESIAN_POINT('',(0.,8.47747275224749,-4.17551861867497));
#59609=CARTESIAN_POINT('',(0.,8.47747275224749,-4.17551861867497));
#59610=CARTESIAN_POINT('',(0.,8.11904715054109,-4.83565645670685));
#59611=CARTESIAN_POINT('',(0.,8.11904715054109,-4.83565645670685));
#59612=CARTESIAN_POINT('',(0.,7.70932198301742,-5.46524057678747));
#59613=CARTESIAN_POINT('',(0.,7.70932198301742,-5.46524057678747));
#59614=CARTESIAN_POINT('',(0.,7.25088606617289,-6.06029300078633));
#59615=CARTESIAN_POINT('',(0.,7.25088606617289,-6.06029300078633));
#59616=CARTESIAN_POINT('',(0.,6.74663599157214,-6.61705393639975));
#59617=CARTESIAN_POINT('',(0.,6.74663599157214,-6.61705393639975));
#59618=CARTESIAN_POINT('',(0.,6.19975782396029,-7.1320055331052));
#59619=CARTESIAN_POINT('',(0.,6.19975782396029,-7.1320055331052));
#59620=CARTESIAN_POINT('',(0.,5.61370697036149,-7.60189410942528));
#59621=CARTESIAN_POINT('',(0.,5.61370697036149,-7.60189410942528));
#59622=CARTESIAN_POINT('',(0.,4.99218634735931,-8.02375071106021));
#59623=CARTESIAN_POINT('',(0.,4.99218634735931,-8.02375071106021));
#59624=CARTESIAN_POINT('',(0.,4.33912298450726,-8.39490986999389));
#59625=CARTESIAN_POINT('',(0.,4.33912298450726,-8.39490986999389));
#59626=CARTESIAN_POINT('',(0.,3.658643211699,-8.71302644604553));
#59627=CARTESIAN_POINT('',(0.,3.658643211699,-8.71302644604553));
#59628=CARTESIAN_POINT('',(0.,2.95504658727499,-8.97609044445489));
#59629=CARTESIAN_POINT('',(0.,2.95504658727499,-8.97609044445489));
#59630=CARTESIAN_POINT('',(0.,2.23277873159856,-9.18243971587732));
#59631=CARTESIAN_POINT('',(0.,2.23277873159856,-9.18243971587732));
#59632=CARTESIAN_POINT('',(0.,1.49640323775065,-9.33077045854464));
#59633=CARTESIAN_POINT('',(0.,1.49640323775065,-9.33077045854464));
#59634=CARTESIAN_POINT('',(0.,0.750572836823028,-9.42014545623492));
#59635=CARTESIAN_POINT('',(0.,0.750572836823028,-9.42014545623492));
#59636=CARTESIAN_POINT('',(0.,-1.73593683779137E-15,-9.45));
#59637=CARTESIAN_POINT('',(0.,-1.73593683779137E-15,-9.45));
#59638=CARTESIAN_POINT('',(0.,-0.750572836823032,-9.42014545623492));
#59639=CARTESIAN_POINT('',(0.,-0.750572836823032,-9.42014545623492));
#59640=CARTESIAN_POINT('',(0.,-1.49640323775065,-9.33077045854464));
#59641=CARTESIAN_POINT('',(0.,-1.49640323775065,-9.33077045854464));
#59642=CARTESIAN_POINT('',(0.,-2.23277873159856,-9.18243971587732));
#59643=CARTESIAN_POINT('',(0.,-2.23277873159856,-9.18243971587732));
#59644=CARTESIAN_POINT('',(0.,-2.95504658727499,-8.97609044445489));
#59645=CARTESIAN_POINT('',(0.,-2.95504658727499,-8.97609044445489));
#59646=CARTESIAN_POINT('',(0.,-3.65864321169901,-8.71302644604553));
#59647=CARTESIAN_POINT('',(0.,-3.65864321169901,-8.71302644604553));
#59648=CARTESIAN_POINT('',(0.,-4.33912298450726,-8.39490986999389));
#59649=CARTESIAN_POINT('',(0.,-4.33912298450726,-8.39490986999389));
#59650=CARTESIAN_POINT('',(0.,-4.99218634735932,-8.02375071106021));
#59651=CARTESIAN_POINT('',(0.,-4.99218634735932,-8.02375071106021));
#59652=CARTESIAN_POINT('',(0.,-5.6137069703615,-7.60189410942528));
#59653=CARTESIAN_POINT('',(0.,-5.6137069703615,-7.60189410942528));
#59654=CARTESIAN_POINT('',(0.,-6.1997578239603,-7.13200553310519));
#59655=CARTESIAN_POINT('',(0.,-6.1997578239603,-7.13200553310519));
#59656=CARTESIAN_POINT('',(0.,-6.74663599157215,-6.61705393639974));
#59657=CARTESIAN_POINT('',(0.,-6.74663599157215,-6.61705393639974));
#59658=CARTESIAN_POINT('',(0.,-7.2508860661729,-6.06029300078632));
#59659=CARTESIAN_POINT('',(0.,-7.2508860661729,-6.06029300078632));
#59660=CARTESIAN_POINT('',(0.,-7.70932198301743,-5.46524057678747));
#59661=CARTESIAN_POINT('',(0.,-7.70932198301743,-5.46524057678747));
#59662=CARTESIAN_POINT('',(0.,-8.11904715054109,-4.83565645670684));
#59663=CARTESIAN_POINT('',(0.,-8.11904715054109,-4.83565645670684));
#59664=CARTESIAN_POINT('',(0.,-8.47747275224749,-4.17551861867497));
#59665=CARTESIAN_POINT('',(0.,-8.47747275224749,-4.17551861867497));
#59666=CARTESIAN_POINT('',(0.,-8.78233410394347,-3.48899809210486));
#59667=CARTESIAN_POINT('',(0.,-8.78233410394347,-3.48899809210486));
#59668=CARTESIAN_POINT('',(0.,-9.03170496296946,-2.7804326033682));
#59669=CARTESIAN_POINT('',(0.,-9.03170496296946,-2.7804326033682));
#59670=CARTESIAN_POINT('',(0.,-9.22400969901338,-2.0542991682097));
#59671=CARTESIAN_POINT('',(0.,-9.22400969901338,-2.0542991682097));
#59672=CARTESIAN_POINT('',(0.,-9.35803324960784,-1.31518580407261));
#59673=CARTESIAN_POINT('',(0.,-9.35803324960784,-1.31518580407261));
#59674=CARTESIAN_POINT('',(0.,-9.43292879740749,-0.567762541068457));
#59675=CARTESIAN_POINT('',(0.,-9.43292879740749,-0.567762541068457));
#59676=CARTESIAN_POINT('',(0.,-9.44822312073834,0.183248085243744));
#59677=CARTESIAN_POINT('',(0.,-9.44822312073834,0.183248085243744));
#59678=CARTESIAN_POINT('',(0.,-9.40381958361198,0.933100872829854));
#59679=CARTESIAN_POINT('',(0.,-9.40381958361198,0.933100872829854));
#59680=CARTESIAN_POINT('',(0.,-9.29999874631253,1.67705793536938));
#59681=CARTESIAN_POINT('',(0.,-9.29999874631253,1.67705793536938));
#59682=CARTESIAN_POINT('',(0.,-9.13741659269838,2.41041863822042));
#59683=CARTESIAN_POINT('',(0.,-9.13741659269838,2.41041863822042));
#59684=CARTESIAN_POINT('',(0.,-8.91710038541936,3.12854929901286));
#59685=CARTESIAN_POINT('',(0.,-8.91710038541936,3.12854929901286));
#59686=CARTESIAN_POINT('',(0.,-8.64044217523789,3.82691246520877));
#59687=CARTESIAN_POINT('',(0.,-8.64044217523789,3.82691246520877));
#59688=CARTESIAN_POINT('',(0.,-8.30919000546483,4.5010955836422));
#59689=CARTESIAN_POINT('',(0.,-8.30919000546483,4.5010955836422));
#59690=CARTESIAN_POINT('',(0.,-7.92543686708426,5.14683888089201));
#59691=CARTESIAN_POINT('',(0.,-7.92543686708426,5.14683888089201));
#59692=CARTESIAN_POINT('',(0.,-7.49160747435326,5.76006227832776));
#59693=CARTESIAN_POINT('',(0.,-7.49160747435326,5.76006227832776));
#59694=CARTESIAN_POINT('',(0.,-7.01044294443414,6.33689117176819));
#59695=CARTESIAN_POINT('',(0.,-7.01044294443414,6.33689117176819));
#59696=CARTESIAN_POINT('',(0.,-6.48498347785953,6.87368091286531));
#59697=CARTESIAN_POINT('',(0.,-6.48498347785953,6.87368091286531));
#59698=CARTESIAN_POINT('',(0.,-5.91854914926258,7.36703983753062));
#59699=CARTESIAN_POINT('',(0.,-5.91854914926258,7.36703983753062));
#59700=CARTESIAN_POINT('',(0.,-5.31471892974448,7.81385069589992));
#59701=CARTESIAN_POINT('',(0.,-5.31471892974448,7.81385069589992));
#59702=CARTESIAN_POINT('',(0.,-4.67730807342486,8.21129034843335));
#59703=CARTESIAN_POINT('',(0.,-4.67730807342486,8.21129034843335));
#59704=CARTESIAN_POINT('',(0.,-4.01034401105639,8.5568476037022));
#59705=CARTESIAN_POINT('',(0.,-4.01034401105639,8.5568476037022));
#59706=CARTESIAN_POINT('',(0.,-3.31804090301785,8.84833908515606));
#59707=CARTESIAN_POINT('',(0.,-3.31804090301785,8.84833908515606));
#59708=CARTESIAN_POINT('',(0.,-2.60477301247064,9.08392302661711));
#59709=CARTESIAN_POINT('',(0.,2.88925991435643,7.72529047046021));
#59710=CARTESIAN_POINT('Origin',(0.,2.88925991435643,6.97529047046021));
#59711=CARTESIAN_POINT('Origin',(0.9,-2.88925991435643,6.97529047046021));
#59712=CARTESIAN_POINT('',(1.,-2.88925991435643,7.72529047046022));
#59713=CARTESIAN_POINT('Origin',(1.,-2.88925991435643,6.97529047046021));
#59714=CARTESIAN_POINT('',(0.9,-2.88925991435643,7.62529047046022));
#59715=CARTESIAN_POINT('Origin',(1.,0.,-0.183038486691444));
#59716=CARTESIAN_POINT('',(1.,-1.84677028397389,6.44045336278674));
#59717=CARTESIAN_POINT('',(1.,-2.60477301247064,9.08392302661711));
#59718=CARTESIAN_POINT('',(1.,-1.84677028397389,6.44045336278674));
#59719=CARTESIAN_POINT('',(1.,-3.31804090301785,8.84833908515606));
#59720=CARTESIAN_POINT('',(1.,-2.60477301247064,9.08392302661711));
#59721=CARTESIAN_POINT('',(1.,-4.01034401105639,8.5568476037022));
#59722=CARTESIAN_POINT('',(1.,-3.31804090301785,8.84833908515606));
#59723=CARTESIAN_POINT('',(1.,-4.67730807342486,8.21129034843335));
#59724=CARTESIAN_POINT('',(1.,-4.01034401105639,8.5568476037022));
#59725=CARTESIAN_POINT('',(1.,-5.31471892974448,7.81385069589992));
#59726=CARTESIAN_POINT('',(1.,-4.67730807342486,8.21129034843335));
#59727=CARTESIAN_POINT('',(1.,-5.91854914926258,7.36703983753062));
#59728=CARTESIAN_POINT('',(1.,-5.31471892974448,7.81385069589992));
#59729=CARTESIAN_POINT('',(1.,-6.48498347785953,6.87368091286531));
#59730=CARTESIAN_POINT('',(1.,-5.91854914926258,7.36703983753062));
#59731=CARTESIAN_POINT('',(1.,-7.01044294443414,6.33689117176819));
#59732=CARTESIAN_POINT('',(1.,-6.48498347785953,6.87368091286531));
#59733=CARTESIAN_POINT('',(1.,-7.49160747435326,5.76006227832776));
#59734=CARTESIAN_POINT('',(1.,-7.01044294443414,6.33689117176819));
#59735=CARTESIAN_POINT('',(1.,-7.92543686708425,5.14683888089201));
#59736=CARTESIAN_POINT('',(1.,-7.49160747435326,5.76006227832776));
#59737=CARTESIAN_POINT('',(1.,-8.30919000546483,4.5010955836422));
#59738=CARTESIAN_POINT('',(1.,-7.92543686708426,5.14683888089201));
#59739=CARTESIAN_POINT('',(1.,-8.64044217523789,3.82691246520877));
#59740=CARTESIAN_POINT('',(1.,-8.30919000546483,4.5010955836422));
#59741=CARTESIAN_POINT('',(1.,-8.91710038541936,3.12854929901286));
#59742=CARTESIAN_POINT('',(1.,-8.64044217523789,3.82691246520877));
#59743=CARTESIAN_POINT('',(1.,-9.13741659269838,2.41041863822042));
#59744=CARTESIAN_POINT('',(1.,-8.91710038541936,3.12854929901286));
#59745=CARTESIAN_POINT('',(1.,-9.29999874631253,1.67705793536937));
#59746=CARTESIAN_POINT('',(1.,-9.13741659269838,2.41041863822042));
#59747=CARTESIAN_POINT('',(1.,-9.40381958361198,0.933100872829854));
#59748=CARTESIAN_POINT('',(1.,-9.29999874631253,1.67705793536938));
#59749=CARTESIAN_POINT('',(1.,-9.44822312073834,0.183248085243743));
#59750=CARTESIAN_POINT('',(1.,-9.40381958361198,0.933100872829854));
#59751=CARTESIAN_POINT('',(1.,-9.43292879740749,-0.567762541068457));
#59752=CARTESIAN_POINT('',(1.,-9.44822312073834,0.183248085243744));
#59753=CARTESIAN_POINT('',(1.,-9.35803324960784,-1.31518580407261));
#59754=CARTESIAN_POINT('',(1.,-9.43292879740749,-0.567762541068457));
#59755=CARTESIAN_POINT('',(1.,-9.22400969901338,-2.0542991682097));
#59756=CARTESIAN_POINT('',(1.,-9.35803324960784,-1.31518580407261));
#59757=CARTESIAN_POINT('',(1.,-9.03170496296946,-2.7804326033682));
#59758=CARTESIAN_POINT('',(1.,-9.22400969901338,-2.0542991682097));
#59759=CARTESIAN_POINT('',(1.,-8.78233410394347,-3.48899809210486));
#59760=CARTESIAN_POINT('',(1.,-9.03170496296946,-2.7804326033682));
#59761=CARTESIAN_POINT('',(1.,-8.47747275224749,-4.17551861867497));
#59762=CARTESIAN_POINT('',(1.,-8.78233410394347,-3.48899809210486));
#59763=CARTESIAN_POINT('',(1.,-8.11904715054109,-4.83565645670684));
#59764=CARTESIAN_POINT('',(1.,-8.47747275224749,-4.17551861867497));
#59765=CARTESIAN_POINT('',(1.,-7.70932198301743,-5.46524057678747));
#59766=CARTESIAN_POINT('',(1.,-8.11904715054109,-4.83565645670684));
#59767=CARTESIAN_POINT('',(1.,-7.2508860661729,-6.06029300078632));
#59768=CARTESIAN_POINT('',(1.,-7.70932198301743,-5.46524057678747));
#59769=CARTESIAN_POINT('',(1.,-6.74663599157215,-6.61705393639974));
#59770=CARTESIAN_POINT('',(1.,-7.2508860661729,-6.06029300078632));
#59771=CARTESIAN_POINT('',(1.,-6.1997578239603,-7.13200553310519));
#59772=CARTESIAN_POINT('',(1.,-6.74663599157215,-6.61705393639974));
#59773=CARTESIAN_POINT('',(1.,-5.6137069703615,-7.60189410942528));
#59774=CARTESIAN_POINT('',(1.,-6.1997578239603,-7.13200553310519));
#59775=CARTESIAN_POINT('',(1.,-4.99218634735932,-8.02375071106021));
#59776=CARTESIAN_POINT('',(1.,-5.6137069703615,-7.60189410942528));
#59777=CARTESIAN_POINT('',(1.,-4.33912298450726,-8.39490986999389));
#59778=CARTESIAN_POINT('',(1.,-4.99218634735932,-8.02375071106021));
#59779=CARTESIAN_POINT('',(1.,-3.65864321169901,-8.71302644604553));
#59780=CARTESIAN_POINT('',(1.,-4.33912298450726,-8.39490986999389));
#59781=CARTESIAN_POINT('',(1.,-2.95504658727499,-8.97609044445489));
#59782=CARTESIAN_POINT('',(1.,-3.65864321169901,-8.71302644604553));
#59783=CARTESIAN_POINT('',(1.,-2.23277873159856,-9.18243971587732));
#59784=CARTESIAN_POINT('',(1.,-2.95504658727499,-8.97609044445489));
#59785=CARTESIAN_POINT('',(1.,-1.49640323775065,-9.33077045854464));
#59786=CARTESIAN_POINT('',(1.,-2.23277873159856,-9.18243971587732));
#59787=CARTESIAN_POINT('',(1.,-0.750572836823032,-9.42014545623492));
#59788=CARTESIAN_POINT('',(1.,-1.49640323775065,-9.33077045854464));
#59789=CARTESIAN_POINT('',(1.,-1.66533453693773E-15,-9.45));
#59790=CARTESIAN_POINT('',(1.,-0.750572836823032,-9.42014545623492));
#59791=CARTESIAN_POINT('',(1.,0.750572836823029,-9.42014545623492));
#59792=CARTESIAN_POINT('',(1.,-1.73593683779137E-15,-9.45));
#59793=CARTESIAN_POINT('',(1.,1.49640323775065,-9.33077045854464));
#59794=CARTESIAN_POINT('',(1.,0.750572836823028,-9.42014545623492));
#59795=CARTESIAN_POINT('',(1.,2.23277873159856,-9.18243971587732));
#59796=CARTESIAN_POINT('',(1.,1.49640323775065,-9.33077045854464));
#59797=CARTESIAN_POINT('',(1.,2.95504658727499,-8.9760904444549));
#59798=CARTESIAN_POINT('',(1.,2.23277873159856,-9.18243971587732));
#59799=CARTESIAN_POINT('',(1.,3.658643211699,-8.71302644604553));
#59800=CARTESIAN_POINT('',(1.,2.95504658727499,-8.97609044445489));
#59801=CARTESIAN_POINT('',(1.,4.33912298450726,-8.39490986999389));
#59802=CARTESIAN_POINT('',(1.,3.658643211699,-8.71302644604553));
#59803=CARTESIAN_POINT('',(1.,4.99218634735931,-8.02375071106021));
#59804=CARTESIAN_POINT('',(1.,4.33912298450726,-8.39490986999389));
#59805=CARTESIAN_POINT('',(1.,5.6137069703615,-7.60189410942528));
#59806=CARTESIAN_POINT('',(1.,4.99218634735931,-8.02375071106021));
#59807=CARTESIAN_POINT('',(1.,6.19975782396029,-7.1320055331052));
#59808=CARTESIAN_POINT('',(1.,5.61370697036149,-7.60189410942528));
#59809=CARTESIAN_POINT('',(1.,6.74663599157214,-6.61705393639975));
#59810=CARTESIAN_POINT('',(1.,6.19975782396029,-7.1320055331052));
#59811=CARTESIAN_POINT('',(1.,7.25088606617289,-6.06029300078633));
#59812=CARTESIAN_POINT('',(1.,6.74663599157214,-6.61705393639975));
#59813=CARTESIAN_POINT('',(1.,7.70932198301742,-5.46524057678747));
#59814=CARTESIAN_POINT('',(1.,7.25088606617289,-6.06029300078633));
#59815=CARTESIAN_POINT('',(1.,8.11904715054109,-4.83565645670685));
#59816=CARTESIAN_POINT('',(1.,7.70932198301742,-5.46524057678747));
#59817=CARTESIAN_POINT('',(1.,8.47747275224749,-4.17551861867497));
#59818=CARTESIAN_POINT('',(1.,8.11904715054109,-4.83565645670685));
#59819=CARTESIAN_POINT('',(1.,8.78233410394347,-3.48899809210487));
#59820=CARTESIAN_POINT('',(1.,8.47747275224749,-4.17551861867497));
#59821=CARTESIAN_POINT('',(1.,9.03170496296946,-2.7804326033682));
#59822=CARTESIAN_POINT('',(1.,8.78233410394347,-3.48899809210487));
#59823=CARTESIAN_POINT('',(1.,9.22400969901338,-2.05429916820971));
#59824=CARTESIAN_POINT('',(1.,9.03170496296946,-2.7804326033682));
#59825=CARTESIAN_POINT('',(1.,9.35803324960784,-1.31518580407262));
#59826=CARTESIAN_POINT('',(1.,9.22400969901338,-2.05429916820971));
#59827=CARTESIAN_POINT('',(1.,9.43292879740749,-0.567762541068465));
#59828=CARTESIAN_POINT('',(1.,9.35803324960784,-1.31518580407262));
#59829=CARTESIAN_POINT('',(1.,9.44822312073834,0.183248085243736));
#59830=CARTESIAN_POINT('',(1.,9.43292879740749,-0.567762541068464));
#59831=CARTESIAN_POINT('',(1.,9.40381958361198,0.933100872829846));
#59832=CARTESIAN_POINT('',(1.,9.44822312073834,0.183248085243736));
#59833=CARTESIAN_POINT('',(1.,9.29999874631253,1.67705793536937));
#59834=CARTESIAN_POINT('',(1.,9.40381958361198,0.933100872829846));
#59835=CARTESIAN_POINT('',(1.,9.13741659269838,2.41041863822041));
#59836=CARTESIAN_POINT('',(1.,9.29999874631253,1.67705793536937));
#59837=CARTESIAN_POINT('',(1.,8.91710038541937,3.12854929901285));
#59838=CARTESIAN_POINT('',(1.,9.13741659269838,2.41041863822041));
#59839=CARTESIAN_POINT('',(1.,8.6404421752379,3.82691246520876));
#59840=CARTESIAN_POINT('',(1.,8.91710038541937,3.12854929901285));
#59841=CARTESIAN_POINT('',(1.,8.30919000546483,4.5010955836422));
#59842=CARTESIAN_POINT('',(1.,8.6404421752379,3.82691246520876));
#59843=CARTESIAN_POINT('',(1.,7.92543686708426,5.146838880892));
#59844=CARTESIAN_POINT('',(1.,8.30919000546483,4.5010955836422));
#59845=CARTESIAN_POINT('',(1.,7.49160747435326,5.76006227832775));
#59846=CARTESIAN_POINT('',(1.,7.92543686708426,5.146838880892));
#59847=CARTESIAN_POINT('',(1.,7.01044294443415,6.33689117176818));
#59848=CARTESIAN_POINT('',(1.,7.49160747435326,5.76006227832775));
#59849=CARTESIAN_POINT('',(1.,6.48498347785954,6.87368091286531));
#59850=CARTESIAN_POINT('',(1.,7.01044294443415,6.33689117176818));
#59851=CARTESIAN_POINT('',(1.,5.91854914926258,7.36703983753062));
#59852=CARTESIAN_POINT('',(1.,6.48498347785954,6.87368091286531));
#59853=CARTESIAN_POINT('',(1.,5.31471892974448,7.81385069589992));
#59854=CARTESIAN_POINT('',(1.,5.91854914926258,7.36703983753062));
#59855=CARTESIAN_POINT('',(1.,4.67730807342487,8.21129034843334));
#59856=CARTESIAN_POINT('',(1.,5.31471892974448,7.81385069589992));
#59857=CARTESIAN_POINT('',(1.,4.0103440110564,8.5568476037022));
#59858=CARTESIAN_POINT('',(1.,4.67730807342487,8.21129034843334));
#59859=CARTESIAN_POINT('',(1.,3.31804090301786,8.84833908515606));
#59860=CARTESIAN_POINT('',(1.,4.0103440110564,8.5568476037022));
#59861=CARTESIAN_POINT('',(1.,2.60477301247065,9.08392302661711));
#59862=CARTESIAN_POINT('',(1.,3.31804090301786,8.84833908515606));
#59863=CARTESIAN_POINT('',(1.,1.8467702839739,6.44045336278674));
#59864=CARTESIAN_POINT('',(1.,2.60477301247065,9.08392302661711));
#59865=CARTESIAN_POINT('',(1.,3.24822445565046,5.85995203783395));
#59866=CARTESIAN_POINT('',(1.,1.8467702839739,6.44045336278674));
#59867=CARTESIAN_POINT('',(1.,3.8784769619707,6.99695765711516));
#59868=CARTESIAN_POINT('',(1.,3.24822445565046,5.85995203783395));
#59869=CARTESIAN_POINT('',(1.,4.37985668768992,6.69453922202999));
#59870=CARTESIAN_POINT('',(1.,3.8784769619707,6.99695765711516));
#59871=CARTESIAN_POINT('',(1.,4.85777416858264,6.35625912994831));
#59872=CARTESIAN_POINT('',(1.,4.37985668768992,6.69453922202999));
#59873=CARTESIAN_POINT('',(1.,5.30966927135158,5.98392949731736));
#59874=CARTESIAN_POINT('',(1.,4.85777416858264,6.35625912994831));
#59875=CARTESIAN_POINT('',(1.,5.73312126073229,5.57954483893976));
#59876=CARTESIAN_POINT('',(1.,5.30966927135158,5.98392949731736));
#59877=CARTESIAN_POINT('',(1.,6.12586176701418,5.14527138365256));
#59878=CARTESIAN_POINT('',(1.,5.73312126073229,5.57954483893976));
#59879=CARTESIAN_POINT('',(1.,6.4857869373617,4.68343547015952));
#59880=CARTESIAN_POINT('',(1.,6.12586176701418,5.14527138365256));
#59881=CARTESIAN_POINT('',(1.,6.81096870584301,4.19651108517863));
#59882=CARTESIAN_POINT('',(1.,6.4857869373617,4.68343547015952));
#59883=CARTESIAN_POINT('',(1.,7.09966512179414,3.68710661066097));
#59884=CARTESIAN_POINT('',(1.,6.81096870584301,4.19651108517863));
#59885=CARTESIAN_POINT('',(1.,7.35032968119119,3.15795085107413));
#59886=CARTESIAN_POINT('',(1.,7.09966512179414,3.68710661066097));
#59887=CARTESIAN_POINT('',(1.,7.5616196110438,2.61187841560012));
#59888=CARTESIAN_POINT('',(1.,7.35032968119119,3.15795085107413));
#59889=CARTESIAN_POINT('',(1.,7.73240306243155,2.05181453355297));
#59890=CARTESIAN_POINT('',(1.,7.5616196110438,2.61187841560012));
#59891=CARTESIAN_POINT('',(1.,7.86176517365131,1.48075938435771));
#59892=CARTESIAN_POINT('',(1.,7.73240306243155,2.05181453355297));
#59893=CARTESIAN_POINT('',(1.,7.94901297099613,0.901772026032747));
#59894=CARTESIAN_POINT('',(1.,7.86176517365131,1.48075938435771));
#59895=CARTESIAN_POINT('',(1.,7.99367908091301,0.317954008268194));
#59896=CARTESIAN_POINT('',(1.,7.94901297099613,0.901772026032747));
#59897=CARTESIAN_POINT('',(1.,7.99552423365383,-0.267567242117314));
#59898=CARTESIAN_POINT('',(1.,7.99367908091301,0.317954008268194));
#59899=CARTESIAN_POINT('',(1.,7.95453854500815,-0.851655174339753));
#59900=CARTESIAN_POINT('',(1.,7.99552423365383,-0.267567242117314));
#59901=CARTESIAN_POINT('',(1.,7.87094156925134,-1.43118091568862));
#59902=CARTESIAN_POINT('',(1.,7.95453854500815,-0.851655174339752));
#59903=CARTESIAN_POINT('',(1.,7.74518112302486,-2.00304003243554));
#59904=CARTESIAN_POINT('',(1.,7.87094156925134,-1.43118091568862));
#59905=CARTESIAN_POINT('',(1.,7.5779308864487,-2.56416915982678));
#59906=CARTESIAN_POINT('',(1.,7.74518112302486,-2.00304003243554));
#59907=CARTESIAN_POINT('',(1.,7.37008679431654,-3.11156241207547));
#59908=CARTESIAN_POINT('',(1.,7.5779308864487,-2.56416915982678));
#59909=CARTESIAN_POINT('',(1.,7.12276223670551,-3.64228748444737));
#59910=CARTESIAN_POINT('',(1.,7.37008679431654,-3.11156241207547));
#59911=CARTESIAN_POINT('',(1.,6.83728209471014,-4.15350136118385));
#59912=CARTESIAN_POINT('',(1.,7.12276223670551,-3.64228748444737));
#59913=CARTESIAN_POINT('',(1.,6.51517564325019,-4.64246554511711));
#59914=CARTESIAN_POINT('',(1.,6.83728209471014,-4.15350136118385));
#59915=CARTESIAN_POINT('',(1.,6.15816835897094,-5.10656072739463));
#59916=CARTESIAN_POINT('',(1.,6.51517564325019,-4.64246554511711));
#59917=CARTESIAN_POINT('',(1.,5.76817267711992,-5.54330081872951));
#59918=CARTESIAN_POINT('',(1.,6.15816835897094,-5.10656072739463));
#59919=CARTESIAN_POINT('',(1.,5.34727774691393,-5.95034626701329));
#59920=CARTESIAN_POINT('',(1.,5.76817267711992,-5.54330081872951));
#59921=CARTESIAN_POINT('',(1.,4.89773824027559,-6.32551658995075));
#59922=CARTESIAN_POINT('',(1.,5.34727774691393,-5.95034626701329));
#59923=CARTESIAN_POINT('',(1.,4.42196227388906,-6.66680205558121));
#59924=CARTESIAN_POINT('',(1.,4.89773824027559,-6.32551658995075));
#59925=CARTESIAN_POINT('',(1.,3.922498509275,-6.97237444811561));
#59926=CARTESIAN_POINT('',(1.,4.42196227388906,-6.66680205558121));
#59927=CARTESIAN_POINT('',(1.,3.40202249998754,-7.24059686141816));
#59928=CARTESIAN_POINT('',(1.,3.922498509275,-6.97237444811561));
#59929=CARTESIAN_POINT('',(1.,2.86332235906941,-7.47003246767062));
#59930=CARTESIAN_POINT('',(1.,3.40202249998754,-7.24059686141816));
#59931=CARTESIAN_POINT('',(1.,2.30928382354251,-7.65945221424645));
#59932=CARTESIAN_POINT('',(1.,2.86332235906941,-7.47003246767062));
#59933=CARTESIAN_POINT('',(1.,1.74287479594128,-7.80784140756411));
#59934=CARTESIAN_POINT('',(1.,2.30928382354251,-7.65945221424645));
#59935=CARTESIAN_POINT('',(1.,1.16712944569751,-7.91440514865052));
#59936=CARTESIAN_POINT('',(1.,1.74287479594128,-7.80784140756411));
#59937=CARTESIAN_POINT('',(1.,0.585131955543308,-7.9785725912974));
#59938=CARTESIAN_POINT('',(1.,1.16712944569752,-7.91440514865052));
#59939=CARTESIAN_POINT('',(1.,-1.38777878078145E-15,-8.));
#59940=CARTESIAN_POINT('',(1.,0.585131955543308,-7.9785725912974));
#59941=CARTESIAN_POINT('',(1.,-0.585131955543311,-7.9785725912974));
#59942=CARTESIAN_POINT('',(1.,-1.46957615897682E-15,-8.));
#59943=CARTESIAN_POINT('',(1.,-1.16712944569752,-7.91440514865052));
#59944=CARTESIAN_POINT('',(1.,-0.585131955543311,-7.9785725912974));
#59945=CARTESIAN_POINT('',(1.,-1.74287479594128,-7.80784140756411));
#59946=CARTESIAN_POINT('',(1.,-1.16712944569752,-7.91440514865052));
#59947=CARTESIAN_POINT('',(1.,-2.30928382354251,-7.65945221424645));
#59948=CARTESIAN_POINT('',(1.,-1.74287479594128,-7.80784140756411));
#59949=CARTESIAN_POINT('',(1.,-2.86332235906941,-7.47003246767062));
#59950=CARTESIAN_POINT('',(1.,-2.30928382354251,-7.65945221424645));
#59951=CARTESIAN_POINT('',(1.,-3.40202249998754,-7.24059686141816));
#59952=CARTESIAN_POINT('',(1.,-2.86332235906941,-7.47003246767062));
#59953=CARTESIAN_POINT('',(1.,-3.922498509275,-6.9723744481156));
#59954=CARTESIAN_POINT('',(1.,-3.40202249998754,-7.24059686141816));
#59955=CARTESIAN_POINT('',(1.,-4.42196227388907,-6.66680205558121));
#59956=CARTESIAN_POINT('',(1.,-3.922498509275,-6.9723744481156));
#59957=CARTESIAN_POINT('',(1.,-4.89773824027559,-6.32551658995075));
#59958=CARTESIAN_POINT('',(1.,-4.42196227388907,-6.66680205558121));
#59959=CARTESIAN_POINT('',(1.,-5.34727774691394,-5.95034626701329));
#59960=CARTESIAN_POINT('',(1.,-4.89773824027559,-6.32551658995075));
#59961=CARTESIAN_POINT('',(1.,-5.76817267711992,-5.54330081872951));
#59962=CARTESIAN_POINT('',(1.,-5.34727774691394,-5.95034626701329));
#59963=CARTESIAN_POINT('',(1.,-6.15816835897094,-5.10656072739463));
#59964=CARTESIAN_POINT('',(1.,-5.76817267711992,-5.54330081872951));
#59965=CARTESIAN_POINT('',(1.,-6.51517564325019,-4.64246554511711));
#59966=CARTESIAN_POINT('',(1.,-6.15816835897094,-5.10656072739463));
#59967=CARTESIAN_POINT('',(1.,-6.83728209471014,-4.15350136118385));
#59968=CARTESIAN_POINT('',(1.,-6.51517564325019,-4.64246554511711));
#59969=CARTESIAN_POINT('',(1.,-7.12276223670551,-3.64228748444736));
#59970=CARTESIAN_POINT('',(1.,-6.83728209471014,-4.15350136118385));
#59971=CARTESIAN_POINT('',(1.,-7.37008679431654,-3.11156241207547));
#59972=CARTESIAN_POINT('',(1.,-7.12276223670551,-3.64228748444736));
#59973=CARTESIAN_POINT('',(1.,-7.5779308864487,-2.56416915982678));
#59974=CARTESIAN_POINT('',(1.,-7.37008679431654,-3.11156241207547));
#59975=CARTESIAN_POINT('',(1.,-7.74518112302486,-2.00304003243553));
#59976=CARTESIAN_POINT('',(1.,-7.5779308864487,-2.56416915982678));
#59977=CARTESIAN_POINT('',(1.,-7.87094156925134,-1.43118091568862));
#59978=CARTESIAN_POINT('',(1.,-7.74518112302486,-2.00304003243553));
#59979=CARTESIAN_POINT('',(1.,-7.95453854500815,-0.851655174339749));
#59980=CARTESIAN_POINT('',(1.,-7.87094156925134,-1.43118091568862));
#59981=CARTESIAN_POINT('',(1.,-7.99552423365383,-0.26756724211731));
#59982=CARTESIAN_POINT('',(1.,-7.95453854500815,-0.85165517433975));
#59983=CARTESIAN_POINT('',(1.,-7.99367908091301,0.317954008268198));
#59984=CARTESIAN_POINT('',(1.,-7.99552423365383,-0.267567242117311));
#59985=CARTESIAN_POINT('',(1.,-7.94901297099613,0.901772026032757));
#59986=CARTESIAN_POINT('',(1.,-7.99367908091301,0.317954008268197));
#59987=CARTESIAN_POINT('',(1.,-7.86176517365131,1.48075938435771));
#59988=CARTESIAN_POINT('',(1.,-7.94901297099613,0.901772026032757));
#59989=CARTESIAN_POINT('',(1.,-7.73240306243155,2.05181453355296));
#59990=CARTESIAN_POINT('',(1.,-7.86176517365131,1.48075938435772));
#59991=CARTESIAN_POINT('',(1.,-7.5616196110438,2.61187841560012));
#59992=CARTESIAN_POINT('',(1.,-7.73240306243155,2.05181453355296));
#59993=CARTESIAN_POINT('',(1.,-7.35032968119119,3.15795085107414));
#59994=CARTESIAN_POINT('',(1.,-7.5616196110438,2.61187841560012));
#59995=CARTESIAN_POINT('',(1.,-7.09966512179413,3.68710661066098));
#59996=CARTESIAN_POINT('',(1.,-7.35032968119119,3.15795085107414));
#59997=CARTESIAN_POINT('',(1.,-6.81096870584301,4.19651108517864));
#59998=CARTESIAN_POINT('',(1.,-7.09966512179413,3.68710661066098));
#59999=CARTESIAN_POINT('',(1.,-6.4857869373617,4.68343547015952));
#60000=CARTESIAN_POINT('',(1.,-6.81096870584301,4.19651108517864));
#60001=CARTESIAN_POINT('',(1.,-6.12586176701418,5.14527138365256));
#60002=CARTESIAN_POINT('',(1.,-6.4857869373617,4.68343547015952));
#60003=CARTESIAN_POINT('',(1.,-5.73312126073229,5.57954483893977));
#60004=CARTESIAN_POINT('',(1.,-6.12586176701418,5.14527138365256));
#60005=CARTESIAN_POINT('',(1.,-5.30966927135158,5.98392949731736));
#60006=CARTESIAN_POINT('',(1.,-5.73312126073229,5.57954483893977));
#60007=CARTESIAN_POINT('',(1.,-4.85777416858265,6.3562591299483));
#60008=CARTESIAN_POINT('',(1.,-5.30966927135158,5.98392949731736));
#60009=CARTESIAN_POINT('',(1.,-4.37985668768992,6.69453922202999));
#60010=CARTESIAN_POINT('',(1.,-4.85777416858265,6.3562591299483));
#60011=CARTESIAN_POINT('',(1.,-3.8784769619707,6.99695765711517));
#60012=CARTESIAN_POINT('',(1.,-4.37985668768992,6.69453922202999));
#60013=CARTESIAN_POINT('',(1.,-3.24822445565046,5.85995203783395));
#60014=CARTESIAN_POINT('',(1.,-3.8784769619707,6.99695765711517));
#60015=CARTESIAN_POINT('',(1.,-3.24822445565046,5.85995203783395));
#60016=CARTESIAN_POINT('',(1.,2.88925991435643,7.72529047046021));
#60017=CARTESIAN_POINT('Origin',(1.,2.88925991435643,6.97529047046021));
#60018=CARTESIAN_POINT('Origin',(0.1,2.88925991435643,6.97529047046021));
#60019=CARTESIAN_POINT('',(0.2,2.88925991435643,7.52529047046021));
#60020=CARTESIAN_POINT('',(0.1,2.88925991435643,7.62529047046021));
#60021=CARTESIAN_POINT('Origin',(0.2,2.88925991435643,6.97529047046021));
#60022=CARTESIAN_POINT('Origin',(0.,2.88925991435643,6.97529047046021));
#60023=CARTESIAN_POINT('',(0.8,2.88925991435643,7.52529047046021));
#60024=CARTESIAN_POINT('',(0.,2.88925991435643,7.52529047046021));
#60025=CARTESIAN_POINT('Origin',(0.8,2.88925991435643,6.97529047046021));
#60026=CARTESIAN_POINT('Origin',(0.9,2.88925991435643,6.97529047046021));
#60027=CARTESIAN_POINT('',(0.9,2.88925991435643,7.62529047046021));
#60028=CARTESIAN_POINT('Origin',(0.,-3.24822445565046,5.85995203783395));
#60029=CARTESIAN_POINT('',(0.,-1.84677028397389,6.44045336278674));
#60030=CARTESIAN_POINT('',(0.,-3.24822445565046,5.85995203783395));
#60031=CARTESIAN_POINT('Origin',(0.,-3.8784769619707,6.99695765711517));
#60032=CARTESIAN_POINT('',(0.,-3.8784769619707,6.99695765711517));
#60033=CARTESIAN_POINT('Origin',(0.,-4.37985668768992,6.69453922202999));
#60034=CARTESIAN_POINT('',(0.,-4.37985668768992,6.69453922202999));
#60035=CARTESIAN_POINT('Origin',(0.,-4.85777416858265,6.3562591299483));
#60036=CARTESIAN_POINT('',(0.,-4.85777416858265,6.3562591299483));
#60037=CARTESIAN_POINT('Origin',(0.,-5.30966927135158,5.98392949731736));
#60038=CARTESIAN_POINT('',(0.,-5.30966927135158,5.98392949731736));
#60039=CARTESIAN_POINT('Origin',(0.,-5.73312126073229,5.57954483893977));
#60040=CARTESIAN_POINT('',(0.,-5.73312126073229,5.57954483893977));
#60041=CARTESIAN_POINT('Origin',(0.,-6.12586176701418,5.14527138365256));
#60042=CARTESIAN_POINT('',(0.,-6.12586176701418,5.14527138365256));
#60043=CARTESIAN_POINT('Origin',(0.,-6.4857869373617,4.68343547015952));
#60044=CARTESIAN_POINT('',(0.,-6.4857869373617,4.68343547015952));
#60045=CARTESIAN_POINT('Origin',(0.,-6.81096870584301,4.19651108517864));
#60046=CARTESIAN_POINT('',(0.,-6.81096870584301,4.19651108517864));
#60047=CARTESIAN_POINT('Origin',(0.,-7.09966512179413,3.68710661066098));
#60048=CARTESIAN_POINT('',(0.,-7.09966512179413,3.68710661066098));
#60049=CARTESIAN_POINT('Origin',(0.,-7.35032968119119,3.15795085107414));
#60050=CARTESIAN_POINT('',(0.,-7.35032968119119,3.15795085107414));
#60051=CARTESIAN_POINT('Origin',(0.,-7.5616196110438,2.61187841560012));
#60052=CARTESIAN_POINT('',(0.,-7.5616196110438,2.61187841560012));
#60053=CARTESIAN_POINT('Origin',(0.,-7.73240306243155,2.05181453355296));
#60054=CARTESIAN_POINT('',(0.,-7.73240306243155,2.05181453355296));
#60055=CARTESIAN_POINT('Origin',(0.,-7.86176517365131,1.48075938435772));
#60056=CARTESIAN_POINT('',(0.,-7.86176517365131,1.48075938435772));
#60057=CARTESIAN_POINT('Origin',(0.,-7.94901297099613,0.901772026032757));
#60058=CARTESIAN_POINT('',(0.,-7.94901297099613,0.901772026032757));
#60059=CARTESIAN_POINT('Origin',(0.,-7.99367908091301,0.317954008268197));
#60060=CARTESIAN_POINT('',(0.,-7.99367908091301,0.317954008268197));
#60061=CARTESIAN_POINT('Origin',(0.,-7.99552423365383,-0.267567242117311));
#60062=CARTESIAN_POINT('',(0.,-7.99552423365383,-0.267567242117311));
#60063=CARTESIAN_POINT('Origin',(0.,-7.95453854500815,-0.85165517433975));
#60064=CARTESIAN_POINT('',(0.,-7.95453854500815,-0.85165517433975));
#60065=CARTESIAN_POINT('Origin',(0.,-7.87094156925134,-1.43118091568862));
#60066=CARTESIAN_POINT('',(0.,-7.87094156925134,-1.43118091568862));
#60067=CARTESIAN_POINT('Origin',(0.,-7.74518112302486,-2.00304003243553));
#60068=CARTESIAN_POINT('',(0.,-7.74518112302486,-2.00304003243553));
#60069=CARTESIAN_POINT('Origin',(0.,-7.5779308864487,-2.56416915982678));
#60070=CARTESIAN_POINT('',(0.,-7.5779308864487,-2.56416915982678));
#60071=CARTESIAN_POINT('Origin',(0.,-7.37008679431654,-3.11156241207547));
#60072=CARTESIAN_POINT('',(0.,-7.37008679431654,-3.11156241207547));
#60073=CARTESIAN_POINT('Origin',(0.,-7.12276223670551,-3.64228748444736));
#60074=CARTESIAN_POINT('',(0.,-7.12276223670551,-3.64228748444736));
#60075=CARTESIAN_POINT('Origin',(0.,-6.83728209471014,-4.15350136118385));
#60076=CARTESIAN_POINT('',(0.,-6.83728209471014,-4.15350136118385));
#60077=CARTESIAN_POINT('Origin',(0.,-6.51517564325019,-4.64246554511711));
#60078=CARTESIAN_POINT('',(0.,-6.51517564325019,-4.64246554511711));
#60079=CARTESIAN_POINT('Origin',(0.,-6.15816835897094,-5.10656072739463));
#60080=CARTESIAN_POINT('',(0.,-6.15816835897094,-5.10656072739463));
#60081=CARTESIAN_POINT('Origin',(0.,-5.76817267711992,-5.54330081872951));
#60082=CARTESIAN_POINT('',(0.,-5.76817267711992,-5.54330081872951));
#60083=CARTESIAN_POINT('Origin',(0.,-5.34727774691394,-5.95034626701329));
#60084=CARTESIAN_POINT('',(0.,-5.34727774691394,-5.95034626701329));
#60085=CARTESIAN_POINT('Origin',(0.,-4.89773824027559,-6.32551658995075));
#60086=CARTESIAN_POINT('',(0.,-4.89773824027559,-6.32551658995075));
#60087=CARTESIAN_POINT('Origin',(0.,-4.42196227388907,-6.66680205558121));
#60088=CARTESIAN_POINT('',(0.,-4.42196227388907,-6.66680205558121));
#60089=CARTESIAN_POINT('Origin',(0.,-3.922498509275,-6.9723744481156));
#60090=CARTESIAN_POINT('',(0.,-3.922498509275,-6.9723744481156));
#60091=CARTESIAN_POINT('Origin',(0.,-3.40202249998754,-7.24059686141816));
#60092=CARTESIAN_POINT('',(0.,-3.40202249998754,-7.24059686141816));
#60093=CARTESIAN_POINT('Origin',(0.,-2.86332235906941,-7.47003246767062));
#60094=CARTESIAN_POINT('',(0.,-2.86332235906941,-7.47003246767062));
#60095=CARTESIAN_POINT('Origin',(0.,-2.30928382354251,-7.65945221424645));
#60096=CARTESIAN_POINT('',(0.,-2.30928382354251,-7.65945221424645));
#60097=CARTESIAN_POINT('Origin',(0.,-1.74287479594128,-7.80784140756411));
#60098=CARTESIAN_POINT('',(0.,-1.74287479594128,-7.80784140756411));
#60099=CARTESIAN_POINT('Origin',(0.,-1.16712944569752,-7.91440514865052));
#60100=CARTESIAN_POINT('',(0.,-1.16712944569752,-7.91440514865052));
#60101=CARTESIAN_POINT('Origin',(0.,-0.585131955543311,-7.9785725912974));
#60102=CARTESIAN_POINT('',(0.,-0.585131955543311,-7.9785725912974));
#60103=CARTESIAN_POINT('Origin',(0.,-1.46957615897682E-15,-8.));
#60104=CARTESIAN_POINT('',(0.,-1.46957615897682E-15,-8.));
#60105=CARTESIAN_POINT('Origin',(0.,0.585131955543308,-7.9785725912974));
#60106=CARTESIAN_POINT('',(0.,0.585131955543308,-7.9785725912974));
#60107=CARTESIAN_POINT('Origin',(0.,1.16712944569752,-7.91440514865052));
#60108=CARTESIAN_POINT('',(0.,1.16712944569752,-7.91440514865052));
#60109=CARTESIAN_POINT('Origin',(0.,1.74287479594128,-7.80784140756411));
#60110=CARTESIAN_POINT('',(0.,1.74287479594128,-7.80784140756411));
#60111=CARTESIAN_POINT('Origin',(0.,2.30928382354251,-7.65945221424645));
#60112=CARTESIAN_POINT('',(0.,2.30928382354251,-7.65945221424645));
#60113=CARTESIAN_POINT('Origin',(0.,2.86332235906941,-7.47003246767062));
#60114=CARTESIAN_POINT('',(0.,2.86332235906941,-7.47003246767062));
#60115=CARTESIAN_POINT('Origin',(0.,3.40202249998754,-7.24059686141816));
#60116=CARTESIAN_POINT('',(0.,3.40202249998754,-7.24059686141816));
#60117=CARTESIAN_POINT('Origin',(0.,3.922498509275,-6.97237444811561));
#60118=CARTESIAN_POINT('',(0.,3.922498509275,-6.97237444811561));
#60119=CARTESIAN_POINT('Origin',(0.,4.42196227388906,-6.66680205558121));
#60120=CARTESIAN_POINT('',(0.,4.42196227388906,-6.66680205558121));
#60121=CARTESIAN_POINT('Origin',(0.,4.89773824027559,-6.32551658995075));
#60122=CARTESIAN_POINT('',(0.,4.89773824027559,-6.32551658995075));
#60123=CARTESIAN_POINT('Origin',(0.,5.34727774691393,-5.95034626701329));
#60124=CARTESIAN_POINT('',(0.,5.34727774691393,-5.95034626701329));
#60125=CARTESIAN_POINT('Origin',(0.,5.76817267711992,-5.54330081872951));
#60126=CARTESIAN_POINT('',(0.,5.76817267711992,-5.54330081872951));
#60127=CARTESIAN_POINT('Origin',(0.,6.15816835897094,-5.10656072739463));
#60128=CARTESIAN_POINT('',(0.,6.15816835897094,-5.10656072739463));
#60129=CARTESIAN_POINT('Origin',(0.,6.51517564325019,-4.64246554511711));
#60130=CARTESIAN_POINT('',(0.,6.51517564325019,-4.64246554511711));
#60131=CARTESIAN_POINT('Origin',(0.,6.83728209471014,-4.15350136118385));
#60132=CARTESIAN_POINT('',(0.,6.83728209471014,-4.15350136118385));
#60133=CARTESIAN_POINT('Origin',(0.,7.12276223670551,-3.64228748444737));
#60134=CARTESIAN_POINT('',(0.,7.12276223670551,-3.64228748444737));
#60135=CARTESIAN_POINT('Origin',(0.,7.37008679431654,-3.11156241207547));
#60136=CARTESIAN_POINT('',(0.,7.37008679431654,-3.11156241207547));
#60137=CARTESIAN_POINT('Origin',(0.,7.5779308864487,-2.56416915982678));
#60138=CARTESIAN_POINT('',(0.,7.5779308864487,-2.56416915982678));
#60139=CARTESIAN_POINT('Origin',(0.,7.74518112302486,-2.00304003243554));
#60140=CARTESIAN_POINT('',(0.,7.74518112302486,-2.00304003243554));
#60141=CARTESIAN_POINT('Origin',(0.,7.87094156925134,-1.43118091568862));
#60142=CARTESIAN_POINT('',(0.,7.87094156925134,-1.43118091568862));
#60143=CARTESIAN_POINT('Origin',(0.,7.95453854500815,-0.851655174339752));
#60144=CARTESIAN_POINT('',(0.,7.95453854500815,-0.851655174339752));
#60145=CARTESIAN_POINT('Origin',(0.,7.99552423365383,-0.267567242117314));
#60146=CARTESIAN_POINT('',(0.,7.99552423365383,-0.267567242117314));
#60147=CARTESIAN_POINT('Origin',(0.,7.99367908091301,0.317954008268194));
#60148=CARTESIAN_POINT('',(0.,7.99367908091301,0.317954008268194));
#60149=CARTESIAN_POINT('Origin',(0.,7.94901297099613,0.901772026032747));
#60150=CARTESIAN_POINT('',(0.,7.94901297099613,0.901772026032747));
#60151=CARTESIAN_POINT('Origin',(0.,7.86176517365131,1.48075938435771));
#60152=CARTESIAN_POINT('',(0.,7.86176517365131,1.48075938435771));
#60153=CARTESIAN_POINT('Origin',(0.,7.73240306243155,2.05181453355297));
#60154=CARTESIAN_POINT('',(0.,7.73240306243155,2.05181453355297));
#60155=CARTESIAN_POINT('Origin',(0.,7.5616196110438,2.61187841560012));
#60156=CARTESIAN_POINT('',(0.,7.5616196110438,2.61187841560012));
#60157=CARTESIAN_POINT('Origin',(0.,7.35032968119119,3.15795085107413));
#60158=CARTESIAN_POINT('',(0.,7.35032968119119,3.15795085107413));
#60159=CARTESIAN_POINT('Origin',(0.,7.09966512179414,3.68710661066097));
#60160=CARTESIAN_POINT('',(0.,7.09966512179414,3.68710661066097));
#60161=CARTESIAN_POINT('Origin',(0.,6.81096870584301,4.19651108517863));
#60162=CARTESIAN_POINT('',(0.,6.81096870584301,4.19651108517863));
#60163=CARTESIAN_POINT('Origin',(0.,6.4857869373617,4.68343547015952));
#60164=CARTESIAN_POINT('',(0.,6.4857869373617,4.68343547015952));
#60165=CARTESIAN_POINT('Origin',(0.,6.12586176701418,5.14527138365256));
#60166=CARTESIAN_POINT('',(0.,6.12586176701418,5.14527138365256));
#60167=CARTESIAN_POINT('Origin',(0.,5.73312126073229,5.57954483893976));
#60168=CARTESIAN_POINT('',(0.,5.73312126073229,5.57954483893976));
#60169=CARTESIAN_POINT('Origin',(0.,5.30966927135158,5.98392949731736));
#60170=CARTESIAN_POINT('',(0.,5.30966927135158,5.98392949731736));
#60171=CARTESIAN_POINT('Origin',(0.,4.85777416858264,6.35625912994831));
#60172=CARTESIAN_POINT('',(0.,4.85777416858264,6.35625912994831));
#60173=CARTESIAN_POINT('Origin',(0.,4.37985668768992,6.69453922202999));
#60174=CARTESIAN_POINT('',(0.,4.37985668768992,6.69453922202999));
#60175=CARTESIAN_POINT('Origin',(0.,3.8784769619707,6.99695765711516));
#60176=CARTESIAN_POINT('',(0.,3.8784769619707,6.99695765711516));
#60177=CARTESIAN_POINT('Origin',(0.,3.24822445565046,5.85995203783395));
#60178=CARTESIAN_POINT('',(0.,3.24822445565046,5.85995203783395));
#60179=CARTESIAN_POINT('Origin',(0.,1.8467702839739,6.44045336278674));
#60180=CARTESIAN_POINT('',(0.,1.8467702839739,6.44045336278674));
#60181=CARTESIAN_POINT('Origin',(0.,2.60477301247065,9.08392302661711));
#60182=CARTESIAN_POINT('',(0.,2.60477301247065,9.08392302661711));
#60183=CARTESIAN_POINT('Origin',(0.,3.31804090301786,8.84833908515606));
#60184=CARTESIAN_POINT('',(0.,3.31804090301786,8.84833908515606));
#60185=CARTESIAN_POINT('Origin',(0.,4.0103440110564,8.5568476037022));
#60186=CARTESIAN_POINT('',(0.,4.0103440110564,8.5568476037022));
#60187=CARTESIAN_POINT('Origin',(0.,4.67730807342487,8.21129034843334));
#60188=CARTESIAN_POINT('',(0.,4.67730807342487,8.21129034843334));
#60189=CARTESIAN_POINT('Origin',(0.,5.31471892974448,7.81385069589992));
#60190=CARTESIAN_POINT('',(0.,5.31471892974448,7.81385069589992));
#60191=CARTESIAN_POINT('Origin',(0.,5.91854914926258,7.36703983753062));
#60192=CARTESIAN_POINT('',(0.,5.91854914926258,7.36703983753062));
#60193=CARTESIAN_POINT('Origin',(0.,6.48498347785954,6.87368091286531));
#60194=CARTESIAN_POINT('',(0.,6.48498347785954,6.87368091286531));
#60195=CARTESIAN_POINT('Origin',(0.,7.01044294443415,6.33689117176818));
#60196=CARTESIAN_POINT('',(0.,7.01044294443415,6.33689117176818));
#60197=CARTESIAN_POINT('Origin',(0.,7.49160747435326,5.76006227832775));
#60198=CARTESIAN_POINT('',(0.,7.49160747435326,5.76006227832775));
#60199=CARTESIAN_POINT('Origin',(0.,7.92543686708426,5.146838880892));
#60200=CARTESIAN_POINT('',(0.,7.92543686708426,5.146838880892));
#60201=CARTESIAN_POINT('Origin',(0.,8.30919000546483,4.5010955836422));
#60202=CARTESIAN_POINT('',(0.,8.30919000546483,4.5010955836422));
#60203=CARTESIAN_POINT('Origin',(0.,8.6404421752379,3.82691246520876));
#60204=CARTESIAN_POINT('',(0.,8.6404421752379,3.82691246520876));
#60205=CARTESIAN_POINT('Origin',(0.,8.91710038541937,3.12854929901285));
#60206=CARTESIAN_POINT('',(0.,8.91710038541937,3.12854929901285));
#60207=CARTESIAN_POINT('Origin',(0.,9.13741659269838,2.41041863822041));
#60208=CARTESIAN_POINT('',(0.,9.13741659269838,2.41041863822041));
#60209=CARTESIAN_POINT('Origin',(0.,9.29999874631253,1.67705793536937));
#60210=CARTESIAN_POINT('',(0.,9.29999874631253,1.67705793536937));
#60211=CARTESIAN_POINT('Origin',(0.,9.40381958361198,0.933100872829846));
#60212=CARTESIAN_POINT('',(0.,9.40381958361198,0.933100872829846));
#60213=CARTESIAN_POINT('Origin',(0.,9.44822312073834,0.183248085243736));
#60214=CARTESIAN_POINT('',(0.,9.44822312073834,0.183248085243736));
#60215=CARTESIAN_POINT('Origin',(0.,9.43292879740749,-0.567762541068464));
#60216=CARTESIAN_POINT('',(0.,9.43292879740749,-0.567762541068464));
#60217=CARTESIAN_POINT('Origin',(0.,9.35803324960784,-1.31518580407262));
#60218=CARTESIAN_POINT('',(0.,9.35803324960784,-1.31518580407262));
#60219=CARTESIAN_POINT('Origin',(0.,9.22400969901338,-2.05429916820971));
#60220=CARTESIAN_POINT('',(0.,9.22400969901338,-2.05429916820971));
#60221=CARTESIAN_POINT('Origin',(0.,9.03170496296946,-2.7804326033682));
#60222=CARTESIAN_POINT('',(0.,9.03170496296946,-2.7804326033682));
#60223=CARTESIAN_POINT('Origin',(0.,8.78233410394347,-3.48899809210487));
#60224=CARTESIAN_POINT('',(0.,8.78233410394347,-3.48899809210487));
#60225=CARTESIAN_POINT('Origin',(0.,8.47747275224749,-4.17551861867497));
#60226=CARTESIAN_POINT('',(0.,8.47747275224749,-4.17551861867497));
#60227=CARTESIAN_POINT('Origin',(0.,8.11904715054109,-4.83565645670685));
#60228=CARTESIAN_POINT('',(0.,8.11904715054109,-4.83565645670685));
#60229=CARTESIAN_POINT('Origin',(0.,7.70932198301742,-5.46524057678747));
#60230=CARTESIAN_POINT('',(0.,7.70932198301742,-5.46524057678747));
#60231=CARTESIAN_POINT('Origin',(0.,7.25088606617289,-6.06029300078633));
#60232=CARTESIAN_POINT('',(0.,7.25088606617289,-6.06029300078633));
#60233=CARTESIAN_POINT('Origin',(0.,6.74663599157214,-6.61705393639975));
#60234=CARTESIAN_POINT('',(0.,6.74663599157214,-6.61705393639975));
#60235=CARTESIAN_POINT('Origin',(0.,6.19975782396029,-7.1320055331052));
#60236=CARTESIAN_POINT('',(0.,6.19975782396029,-7.1320055331052));
#60237=CARTESIAN_POINT('Origin',(0.,5.61370697036149,-7.60189410942528));
#60238=CARTESIAN_POINT('',(0.,5.61370697036149,-7.60189410942528));
#60239=CARTESIAN_POINT('Origin',(0.,4.99218634735931,-8.02375071106021));
#60240=CARTESIAN_POINT('',(0.,4.99218634735931,-8.02375071106021));
#60241=CARTESIAN_POINT('Origin',(0.,4.33912298450726,-8.39490986999389));
#60242=CARTESIAN_POINT('',(0.,4.33912298450726,-8.39490986999389));
#60243=CARTESIAN_POINT('Origin',(0.,3.658643211699,-8.71302644604553));
#60244=CARTESIAN_POINT('',(0.,3.658643211699,-8.71302644604553));
#60245=CARTESIAN_POINT('Origin',(0.,2.95504658727499,-8.97609044445489));
#60246=CARTESIAN_POINT('',(0.,2.95504658727499,-8.97609044445489));
#60247=CARTESIAN_POINT('Origin',(0.,2.23277873159856,-9.18243971587732));
#60248=CARTESIAN_POINT('',(0.,2.23277873159856,-9.18243971587732));
#60249=CARTESIAN_POINT('Origin',(0.,1.49640323775065,-9.33077045854464));
#60250=CARTESIAN_POINT('',(0.,1.49640323775065,-9.33077045854464));
#60251=CARTESIAN_POINT('Origin',(0.,0.750572836823028,-9.42014545623492));
#60252=CARTESIAN_POINT('',(0.,0.750572836823028,-9.42014545623492));
#60253=CARTESIAN_POINT('Origin',(0.,-1.73593683779137E-15,-9.45));
#60254=CARTESIAN_POINT('',(0.,-1.73593683779137E-15,-9.45));
#60255=CARTESIAN_POINT('Origin',(0.,-0.750572836823032,-9.42014545623492));
#60256=CARTESIAN_POINT('',(0.,-0.750572836823032,-9.42014545623492));
#60257=CARTESIAN_POINT('Origin',(0.,-1.49640323775065,-9.33077045854464));
#60258=CARTESIAN_POINT('',(0.,-1.49640323775065,-9.33077045854464));
#60259=CARTESIAN_POINT('Origin',(0.,-2.23277873159856,-9.18243971587732));
#60260=CARTESIAN_POINT('',(0.,-2.23277873159856,-9.18243971587732));
#60261=CARTESIAN_POINT('Origin',(0.,-2.95504658727499,-8.97609044445489));
#60262=CARTESIAN_POINT('',(0.,-2.95504658727499,-8.97609044445489));
#60263=CARTESIAN_POINT('Origin',(0.,-3.65864321169901,-8.71302644604553));
#60264=CARTESIAN_POINT('',(0.,-3.65864321169901,-8.71302644604553));
#60265=CARTESIAN_POINT('Origin',(0.,-4.33912298450726,-8.39490986999389));
#60266=CARTESIAN_POINT('',(0.,-4.33912298450726,-8.39490986999389));
#60267=CARTESIAN_POINT('Origin',(0.,-4.99218634735932,-8.02375071106021));
#60268=CARTESIAN_POINT('',(0.,-4.99218634735932,-8.02375071106021));
#60269=CARTESIAN_POINT('Origin',(0.,-5.6137069703615,-7.60189410942528));
#60270=CARTESIAN_POINT('',(0.,-5.6137069703615,-7.60189410942528));
#60271=CARTESIAN_POINT('Origin',(0.,-6.1997578239603,-7.13200553310519));
#60272=CARTESIAN_POINT('',(0.,-6.1997578239603,-7.13200553310519));
#60273=CARTESIAN_POINT('Origin',(0.,-6.74663599157215,-6.61705393639974));
#60274=CARTESIAN_POINT('',(0.,-6.74663599157215,-6.61705393639974));
#60275=CARTESIAN_POINT('Origin',(0.,-7.2508860661729,-6.06029300078632));
#60276=CARTESIAN_POINT('',(0.,-7.2508860661729,-6.06029300078632));
#60277=CARTESIAN_POINT('Origin',(0.,-7.70932198301743,-5.46524057678747));
#60278=CARTESIAN_POINT('',(0.,-7.70932198301743,-5.46524057678747));
#60279=CARTESIAN_POINT('Origin',(0.,-8.11904715054109,-4.83565645670684));
#60280=CARTESIAN_POINT('',(0.,-8.11904715054109,-4.83565645670684));
#60281=CARTESIAN_POINT('Origin',(0.,-8.47747275224749,-4.17551861867497));
#60282=CARTESIAN_POINT('',(0.,-8.47747275224749,-4.17551861867497));
#60283=CARTESIAN_POINT('Origin',(0.,-8.78233410394347,-3.48899809210486));
#60284=CARTESIAN_POINT('',(0.,-8.78233410394347,-3.48899809210486));
#60285=CARTESIAN_POINT('Origin',(0.,-9.03170496296946,-2.7804326033682));
#60286=CARTESIAN_POINT('',(0.,-9.03170496296946,-2.7804326033682));
#60287=CARTESIAN_POINT('Origin',(0.,-9.22400969901338,-2.0542991682097));
#60288=CARTESIAN_POINT('',(0.,-9.22400969901338,-2.0542991682097));
#60289=CARTESIAN_POINT('Origin',(0.,-9.35803324960784,-1.31518580407261));
#60290=CARTESIAN_POINT('',(0.,-9.35803324960784,-1.31518580407261));
#60291=CARTESIAN_POINT('Origin',(0.,-9.43292879740749,-0.567762541068457));
#60292=CARTESIAN_POINT('',(0.,-9.43292879740749,-0.567762541068457));
#60293=CARTESIAN_POINT('Origin',(0.,-9.44822312073834,0.183248085243744));
#60294=CARTESIAN_POINT('',(0.,-9.44822312073834,0.183248085243744));
#60295=CARTESIAN_POINT('Origin',(0.,-9.40381958361198,0.933100872829854));
#60296=CARTESIAN_POINT('',(0.,-9.40381958361198,0.933100872829854));
#60297=CARTESIAN_POINT('Origin',(0.,-9.29999874631253,1.67705793536938));
#60298=CARTESIAN_POINT('',(0.,-9.29999874631253,1.67705793536938));
#60299=CARTESIAN_POINT('Origin',(0.,-9.13741659269838,2.41041863822042));
#60300=CARTESIAN_POINT('',(0.,-9.13741659269838,2.41041863822042));
#60301=CARTESIAN_POINT('Origin',(0.,-8.91710038541936,3.12854929901286));
#60302=CARTESIAN_POINT('',(0.,-8.91710038541936,3.12854929901286));
#60303=CARTESIAN_POINT('Origin',(0.,-8.64044217523789,3.82691246520877));
#60304=CARTESIAN_POINT('',(0.,-8.64044217523789,3.82691246520877));
#60305=CARTESIAN_POINT('Origin',(0.,-8.30919000546483,4.5010955836422));
#60306=CARTESIAN_POINT('',(0.,-8.30919000546483,4.5010955836422));
#60307=CARTESIAN_POINT('Origin',(0.,-7.92543686708426,5.14683888089201));
#60308=CARTESIAN_POINT('',(0.,-7.92543686708426,5.14683888089201));
#60309=CARTESIAN_POINT('Origin',(0.,-7.49160747435326,5.76006227832776));
#60310=CARTESIAN_POINT('',(0.,-7.49160747435326,5.76006227832776));
#60311=CARTESIAN_POINT('Origin',(0.,-7.01044294443414,6.33689117176819));
#60312=CARTESIAN_POINT('',(0.,-7.01044294443414,6.33689117176819));
#60313=CARTESIAN_POINT('Origin',(0.,-6.48498347785953,6.87368091286531));
#60314=CARTESIAN_POINT('',(0.,-6.48498347785953,6.87368091286531));
#60315=CARTESIAN_POINT('Origin',(0.,-5.91854914926258,7.36703983753062));
#60316=CARTESIAN_POINT('',(0.,-5.91854914926258,7.36703983753062));
#60317=CARTESIAN_POINT('Origin',(0.,-5.31471892974448,7.81385069589992));
#60318=CARTESIAN_POINT('',(0.,-5.31471892974448,7.81385069589992));
#60319=CARTESIAN_POINT('Origin',(0.,-4.67730807342486,8.21129034843335));
#60320=CARTESIAN_POINT('',(0.,-4.67730807342486,8.21129034843335));
#60321=CARTESIAN_POINT('Origin',(0.,-4.01034401105639,8.5568476037022));
#60322=CARTESIAN_POINT('',(0.,-4.01034401105639,8.5568476037022));
#60323=CARTESIAN_POINT('Origin',(0.,-3.31804090301785,8.84833908515606));
#60324=CARTESIAN_POINT('',(0.,-3.31804090301785,8.84833908515606));
#60325=CARTESIAN_POINT('Origin',(0.,-2.60477301247064,9.08392302661711));
#60326=CARTESIAN_POINT('',(0.,-2.60477301247064,9.08392302661711));
#60327=CARTESIAN_POINT('Origin',(0.,-1.84677028397389,6.44045336278674));
#60352=UNCERTAINTY_MEASURE_WITH_UNIT(LENGTH_MEASURE(0.01),#60366,
'DISTANCE_ACCURACY_VALUE',
'Maximum model space distance between geometric entities at asserted c
onnectivities');
#60353=UNCERTAINTY_MEASURE_WITH_UNIT(LENGTH_MEASURE(0.01),#60366,
'DISTANCE_ACCURACY_VALUE',
'Maximum model space distance between geometric entities at asserted c
onnectivities');
#60364=(
GEOMETRIC_REPRESENTATION_CONTEXT(3)
GLOBAL_UNCERTAINTY_ASSIGNED_CONTEXT((#60352))
GLOBAL_UNIT_ASSIGNED_CONTEXT((#60366,#60368,#60369))
REPRESENTATION_CONTEXT('','3D')
);
#60365=(
GEOMETRIC_REPRESENTATION_CONTEXT(3)
GLOBAL_UNCERTAINTY_ASSIGNED_CONTEXT((#60353))
GLOBAL_UNIT_ASSIGNED_CONTEXT((#60366,#60368,#60369))
REPRESENTATION_CONTEXT('','3D')
);
#60366=(
LENGTH_UNIT()
NAMED_UNIT(*)
SI_UNIT(.MILLI.,.METRE.)
);
#60368=(
NAMED_UNIT(*)
PLANE_ANGLE_UNIT()
SI_UNIT($,.RADIAN.)
);
#60369=(
NAMED_UNIT(*)
SI_UNIT($,.STERADIAN.)
SOLID_ANGLE_UNIT()
);
#60380=SHAPE_DEFINITION_REPRESENTATION(#60391,#60416);
#60391=PRODUCT_DEFINITION_SHAPE('',$,#60428);
#60416=SHAPE_REPRESENTATION('',(#19497),#60364);
#60417=PRODUCT_DEFINITION_CONTEXT('part definition',#60452,'design');
#60428=PRODUCT_DEFINITION('2026-10-25-00-06-28-626',
'04_Journal_Retaining_Ring_D18',#60439,#60417);
#60439=PRODUCT_DEFINITION_FORMATION('',$,#60464);
#60452=APPLICATION_CONTEXT(
'Core Data for Automotive Mechanical Design Process');
#60453=PRODUCT_CONTEXT('part definition',#60452,'mechanical');
#60464=PRODUCT('2026-10-25-00-06-28-626',
'04_Journal_Retaining_Ring_D18',$,(#60453));
#60535=COLOUR_RGB('Off White',0.89,0.88,0.83);
#60536=FILL_AREA_STYLE_COLOUR('',#60535);
#60537=FILL_AREA_STYLE('',(#60536));
#60538=SURFACE_STYLE_FILL_AREA(#60537);
#60539=SURFACE_SIDE_STYLE('',(#60538));
#60540=SURFACE_STYLE_USAGE(.BOTH.,#60539);
#60541=PRESENTATION_STYLE_ASSIGNMENT((#60540));
ENDSEC;
END-ISO-10303-21;
